ISO-10303-21;
HEADER;
FILE_DESCRIPTION (('STEP AP214'),
    '1' );
FILE_NAME ('Insulator.step',
    '2026-10-05T22:38:29',
    ( '' ),
    ( '' ),
    'SwSTEP 2.0',
    'SolidWorks 2020',
    '' );
FILE_SCHEMA (( 'AUTOMOTIVE_DESIGN' ));
ENDSEC;

DATA;
#79=VERTEX_POINT ( 'NONE', #50744 ) ;
#165=ORIENTED_EDGE ( 'NONE', *, *, #34097, .T. ) ;
#199=DIRECTION ( 'NONE',  ( 0.7071067811865462405, 0.7071067811865462405, -6.013987063531392487E-08 ) ) ;
#228=AXIS2_PLACEMENT_3D ( 'NONE', #34366, #45196, #60235 ) ;
#310=DIRECTION ( 'NONE',  ( 1.000000000000000000, 0.000000000000000000, 0.000000000000000000 ) ) ;
#341=ORIENTED_EDGE ( 'NONE', *, *, #30199, .F. ) ;
#514=CARTESIAN_POINT ( 'NONE',  ( 10.90000000000000036, 0.2500000000000000000, 4.902439024389999567 ) ) ;
#592=ORIENTED_EDGE ( 'NONE', *, *, #31679, .T. ) ;
#778=FACE_OUTER_BOUND ( 'NONE', #54702, .T. ) ;
#804=VECTOR ( 'NONE', #57381, 1000.000000000000000 ) ;
#821=DIRECTION ( 'NONE',  ( -0.4384236320214023319, 0.000000000000000000, -0.8987684456439056779 ) ) ;
#907=CARTESIAN_POINT ( 'NONE',  ( 5.100000000000000533, 0.1499999999999999944, 6.463315149415000072 ) ) ;
#1085=VECTOR ( 'NONE', #9254, 1000.000000000000000 ) ;
#1240=EDGE_LOOP ( 'NONE', ( #37312, #27362, #1741, #18662 ) ) ;
#1355=ORIENTED_EDGE ( 'NONE', *, *, #39332, .T. ) ;
#1429=ORIENTED_EDGE ( 'NONE', *, *, #56998, .F. ) ;
#1460=ORIENTED_EDGE ( 'NONE', *, *, #17637, .F. ) ;
#1629=FILL_AREA_STYLE_COLOUR ( '', #4910 ) ;
#1695=ORIENTED_EDGE ( 'NONE', *, *, #30611, .F. ) ;
#1723=ORIENTED_EDGE ( 'NONE', *, *, #16134, .F. ) ;
#1741=ORIENTED_EDGE ( 'NONE', *, *, #35469, .F. ) ;
#1810=CYLINDRICAL_SURFACE ( 'NONE', #28570, 1.050000000000000044 ) ;
#1827=EDGE_CURVE ( 'NONE', #35905, #30122, #41502, .T. ) ;
#1858=CARTESIAN_POINT ( 'NONE',  ( 7.000000000000000000, -9.735955015381000166, -5.735955015381000166 ) ) ;
#2000=CARTESIAN_POINT ( 'NONE',  ( 7.204898016025000018, -0.2500000000000000000, 3.099950251719000072 ) ) ;
#2063=ORIENTED_EDGE ( 'NONE', *, *, #25484, .T. ) ;
#2122=DIRECTION ( 'NONE',  ( 0.000000000000000000, 0.000000000000000000, -1.000000000000000000 ) ) ;
#2135=DIRECTION ( 'NONE',  ( 0.7071067811865473507, 0.7071067811865473507, -2.044918114706133567E-08 ) ) ;
#2140=EDGE_CURVE ( 'NONE', #22158, #29897, #58322, .T. ) ;
#2290=CARTESIAN_POINT ( 'NONE',  ( 5.200000000000000178, 0.8000000000000000444, -3.149999999999999911 ) ) ;
#2319=EDGE_CURVE ( 'NONE', #52012, #63702, #47413, .T. ) ;
#2356=FACE_OUTER_BOUND ( 'NONE', #13486, .T. ) ;
#2357=EDGE_CURVE ( 'NONE', #37496, #5290, #28185, .T. ) ;
#2382=CARTESIAN_POINT ( 'NONE',  ( 5.500000000000000000, 0.5415384615384001288, -2.132307692307999769 ) ) ;
#2424=CARTESIAN_POINT ( 'NONE',  ( 5.000000000000000000, 0.000000000000000000, 0.000000000000000000 ) ) ;
#2476=DIRECTION ( 'NONE',  ( 1.000000000000000000, -2.772811999483000412E-10, 2.750922296957000062E-11 ) ) ;
#2505=CARTESIAN_POINT ( 'NONE',  ( 7.000000000000000000, -9.370210309074998634, -5.370210309075000410 ) ) ;
#2599=EDGE_CURVE ( 'NONE', #35905, #43884, #68338, .T. ) ;
#2630=DIRECTION ( 'NONE',  ( 1.000000000000000000, 0.000000000000000000, 0.000000000000000000 ) ) ;
#2656=DIRECTION ( 'NONE',  ( 0.000000000000000000, 1.000000000000000000, 0.000000000000000000 ) ) ;
#2660=ORIENTED_EDGE ( 'NONE', *, *, #2599, .F. ) ;
#2664=EDGE_CURVE ( 'NONE', #64650, #54437, #48242, .T. ) ;
#2689=ORIENTED_EDGE ( 'NONE', *, *, #5232, .T. ) ;
#2735=DIRECTION ( 'NONE',  ( 0.000000000000000000, -0.7071067811865475727, 0.7071067811865475727 ) ) ;
#2775=ORIENTED_EDGE ( 'NONE', *, *, #15396, .F. ) ;
#2821=ORIENTED_EDGE ( 'NONE', *, *, #65016, .F. ) ;
#2825=CIRCLE ( 'NONE', #13967, 0.5500000000000001554 ) ;
#2837=ORIENTED_EDGE ( 'NONE', *, *, #6291, .T. ) ;
#2841=ORIENTED_EDGE ( 'NONE', *, *, #64153, .F. ) ;
#2856=VECTOR ( 'NONE', #61927, 1000.000000000000000 ) ;
#2920=CARTESIAN_POINT ( 'NONE',  ( 10.90000000000000036, 0.000000000000000000, 0.000000000000000000 ) ) ;
#3101=ORIENTED_EDGE ( 'NONE', *, *, #20313, .T. ) ;
#3110=DIRECTION ( 'NONE',  ( 0.000000000000000000, -1.000000000000000000, 0.000000000000000000 ) ) ;
#3222=ADVANCED_FACE ( 'NONE', ( #65205 ), #40779, .F. ) ;
#3251=DIRECTION ( 'NONE',  ( 0.000000000000000000, -0.1218274111675002047, 0.9925512993736015366 ) ) ;
#3354=EDGE_LOOP ( 'NONE', ( #67265, #60278, #29681, #40410 ) ) ;
#3452=PRESENTATION_STYLE_ASSIGNMENT (( #51695 ) ) ;
#3579=DIRECTION ( 'NONE',  ( 0.7071067811865712205, 0.1740570408699930738, -0.6853496527492721757 ) ) ;
#3605=EDGE_CURVE ( 'NONE', #46374, #38378, #22664, .T. ) ;
#3657=DIRECTION ( 'NONE',  ( 0.000000000000000000, -1.000000000000000000, 0.000000000000000000 ) ) ;
#3659=VERTEX_POINT ( 'NONE', #8132 ) ;
#3682=CARTESIAN_POINT ( 'NONE',  ( 5.200000000000000178, -1.376649746192999846, 11.21582968292000082 ) ) ;
#3689=EDGE_CURVE ( 'NONE', #5290, #13996, #62965, .T. ) ;
#3796=CARTESIAN_POINT ( 'NONE',  ( 5.500000000000000000, 0.000000000000000000, 0.000000000000000000 ) ) ;
#3820=DIRECTION ( 'NONE',  ( 0.000000000000000000, 1.000000000000000000, 0.000000000000000000 ) ) ;
#3851=EDGE_CURVE ( 'NONE', #36962, #18749, #68215, .T. ) ;
#3888=ORIENTED_EDGE ( 'NONE', *, *, #31740, .F. ) ;
#4043=CARTESIAN_POINT ( 'NONE',  ( 5.000000000000000000, -1.199999999999999956, -9.776630298829998011 ) ) ;
#4106=ORIENTED_EDGE ( 'NONE', *, *, #23832, .F. ) ;
#4131=ORIENTED_EDGE ( 'NONE', *, *, #59428, .T. ) ;
#4217=CIRCLE ( 'NONE', #52224, 1.250000000000000000 ) ;
#4394=CARTESIAN_POINT ( 'NONE',  ( 5.200000000000000178, 1.600000000000000089, 0.000000000000000000 ) ) ;
#4445=CARTESIAN_POINT ( 'NONE',  ( 7.000000000000000000, -0.2392304845412999981, -3.000000000000000000 ) ) ;
#4478=DIRECTION ( 'NONE',  ( 1.000000000000000000, 0.000000000000000000, 0.000000000000000000 ) ) ;
#4480=DIRECTION ( 'NONE',  ( 0.000000000000000000, 1.000000000000000000, 0.000000000000000000 ) ) ;
#4545=VERTEX_POINT ( 'NONE', #67544 ) ;
#4548=AXIS2_PLACEMENT_3D ( 'NONE', #18686, #23239, #18345 ) ;
#4616=CARTESIAN_POINT ( 'NONE',  ( 5.200000000000000178, 0.6646153846154000400, -2.616923076922999858 ) ) ;
#4668=CARTESIAN_POINT ( 'NONE',  ( 7.000000000000000000, 0.000000000000000000, 0.000000000000000000 ) ) ;
#4682=DIRECTION ( 'NONE',  ( -1.000000000000000000, 0.000000000000000000, 0.000000000000000000 ) ) ;
#4709=AXIS2_PLACEMENT_3D ( 'NONE', #58932, #21518, #53687 ) ;
#4733=ORIENTED_EDGE ( 'NONE', *, *, #11225, .F. ) ;
#4763=CYLINDRICAL_SURFACE ( 'NONE', #36594, 2.700000000000000178 ) ;
#4856=CONICAL_SURFACE ( 'NONE', #51728, 1.349999999648999971, 0.7853981633972997312 ) ;
#4910=COLOUR_RGB ( '', 0.40784314, 0.44705882, 0.49803922) ;
#5053=DIRECTION ( 'NONE',  ( 0.000000000000000000, -0.9897433186107934544, -0.1428571428570991342 ) ) ;
#5096=DIRECTION ( 'NONE',  ( 0.000000000000000000, 0.2461538461537954858, 0.9692307692307821076 ) ) ;
#5110=DIRECTION ( 'NONE',  ( 0.000000000000000000, 0.000000000000000000, -1.000000000000000000 ) ) ;
#5121=DIRECTION ( 'NONE',  ( 0.000000000000000000, 1.000000000000000000, 0.000000000000000000 ) ) ;
#5133=ORIENTED_EDGE ( 'NONE', *, *, #15265, .T. ) ;
#5148=ORIENTED_EDGE ( 'NONE', *, *, #23832, .T. ) ;
#5201=EDGE_CURVE ( 'NONE', #8285, #32203, #55185, .T. ) ;
#5229=ORIENTED_EDGE ( 'NONE', *, *, #49476, .F. ) ;
#5232=EDGE_CURVE ( 'NONE', #52415, #13624, #25039, .T. ) ;
#5290=VERTEX_POINT ( 'NONE', #4616 ) ;
#5297=VECTOR ( 'NONE', #68800, 1000.000000000000000 ) ;
#5362=ORIENTED_EDGE ( 'NONE', *, *, #48233, .F. ) ;
#5430=DIRECTION ( 'NONE',  ( 1.000000000000000000, 0.000000000000000000, 0.000000000000000000 ) ) ;
#5699=EDGE_LOOP ( 'NONE', ( #50550, #18380, #44001, #64838 ) ) ;
#5737=CARTESIAN_POINT ( 'NONE',  ( 7.000000000000000000, 0.8000000000000000444, 3.149999999999999911 ) ) ;
#5768=CARTESIAN_POINT ( 'NONE',  ( 5.199999999919999283, -1.376649745807000169, 11.21582968289000171 ) ) ;
#5799=DIRECTION ( 'NONE',  ( 0.000000000000000000, -1.000000000000000000, 0.000000000000000000 ) ) ;
#5885=DIRECTION ( 'NONE',  ( -0.000000000000000000, 1.000000000000000000, 0.000000000000000000 ) ) ;
#5980=DIRECTION ( 'NONE',  ( 1.000000000000000000, 0.000000000000000000, 0.000000000000000000 ) ) ;
#6110=VECTOR ( 'NONE', #68345, 1000.000000000000000 ) ;
#6139=STYLED_ITEM ( 'NONE', ( #3452 ), #46907 ) ;
#6142=FACE_OUTER_BOUND ( 'NONE', #58373, .T. ) ;
#6291=EDGE_CURVE ( 'NONE', #16920, #47459, #31743, .T. ) ;
#6304=ORIENTED_EDGE ( 'NONE', *, *, #57227, .T. ) ;
#6385=EDGE_LOOP ( 'NONE', ( #7270, #38058, #26788, #67346, #28623 ) ) ;
#6398=FACE_OUTER_BOUND ( 'NONE', #57113, .T. ) ;
#6437=ORIENTED_EDGE ( 'NONE', *, *, #42579, .T. ) ;
#6538=ORIENTED_EDGE ( 'NONE', *, *, #68170, .F. ) ;
#6675=FACE_OUTER_BOUND ( 'NONE', #57989, .T. ) ;
#6686=EDGE_CURVE ( 'NONE', #37678, #62414, #9282, .T. ) ;
#6725=ORIENTED_EDGE ( 'NONE', *, *, #28353, .T. ) ;
#6747=AXIS2_PLACEMENT_3D ( 'NONE', #68158, #20623, #41947 ) ;
#6803=VECTOR ( 'NONE', #9467, 1000.000000000000114 ) ;
#6841=ORIENTED_EDGE ( 'NONE', *, *, #62668, .T. ) ;
#6855=ORIENTED_EDGE ( 'NONE', *, *, #52410, .T. ) ;
#6865=SURFACE_SIDE_STYLE ('',( #65246 ) ) ;
#6880=EDGE_CURVE ( 'NONE', #44713, #11166, #24526, .T. ) ;
#6898=AXIS2_PLACEMENT_3D ( 'NONE', #33009, #22164, #26391 ) ;
#6912=CIRCLE ( 'NONE', #62747, 1.449999999999999956 ) ;
#7030=CARTESIAN_POINT ( 'NONE',  ( 4.999999999844999543, 0.04999999984535999364, 9.776630291645998838 ) ) ;
#7142=ADVANCED_FACE ( 'NONE', ( #33634 ), #1810, .T. ) ;
#7171=ADVANCED_FACE ( 'NONE', ( #29436 ), #57290, .T. ) ;
#7270=ORIENTED_EDGE ( 'NONE', *, *, #10523, .F. ) ;
#7322=DIRECTION ( 'NONE',  ( 0.000000000000000000, -1.000000000000000000, 0.000000000000000000 ) ) ;
#7503=FACE_OUTER_BOUND ( 'NONE', #38319, .T. ) ;
#7518=DIRECTION ( 'NONE',  ( 0.000000000000000000, 0.000000000000000000, 1.000000000000000000 ) ) ;
#7550=B_SPLINE_CURVE_WITH_KNOTS ( 'NONE', 3,
 ( #4445, #68415, #15297, #19164 ),
 .UNSPECIFIED., .F., .F.,
 ( 4, 4 ),
 ( 0.000000000000000000, 1.000000000000000000 ),
 .UNSPECIFIED. ) ;
#7558=( NAMED_UNIT ( * ) SI_UNIT ( $, .STERADIAN. ) SOLID_ANGLE_UNIT ( ) );
#7589=ORIENTED_EDGE ( 'NONE', *, *, #20910, .T. ) ;
#7597=AXIS2_PLACEMENT_3D ( 'NONE', #11231, #5980, #59817 ) ;
#7629=EDGE_LOOP ( 'NONE', ( #1695, #1355, #8209, #1460, #67568, #48005 ) ) ;
#7720=CARTESIAN_POINT ( 'NONE',  ( 7.000000000000000000, -9.370210309074998634, 5.370210309075000410 ) ) ;
#7751=CARTESIAN_POINT ( 'NONE',  ( 7.000000000000000000, -0.2392304845412999981, 3.000000000000000000 ) ) ;
#7776=AXIS2_PLACEMENT_3D ( 'NONE', #31716, #26121, #42545 ) ;
#7844=ORIENTED_EDGE ( 'NONE', *, *, #54778, .T. ) ;
#7858=DIRECTION ( 'NONE',  ( 0.000000000000000000, -0.8676120656550951882, 0.4972416952847970584 ) ) ;
#7995=VERTEX_POINT ( 'NONE', #64740 ) ;
#8057=VERTEX_POINT ( 'NONE', #12314 ) ;
#8083=AXIS2_PLACEMENT_3D ( 'NONE', #21270, #37350, #58675 ) ;
#8123=DIRECTION ( 'NONE',  ( -1.000000000000000000, 0.000000000000000000, 0.000000000000000000 ) ) ;
#8132=CARTESIAN_POINT ( 'NONE',  ( 10.90000000000000036, -8.263403946409999534, 6.953859016290999229 ) ) ;
#8170=ORIENTED_EDGE ( 'NONE', *, *, #16471, .F. ) ;
#8201=DIRECTION ( 'NONE',  ( 0.000000000000000000, 0.000000000000000000, 1.000000000000000000 ) ) ;
#8209=ORIENTED_EDGE ( 'NONE', *, *, #9564, .F. ) ;
#8228=DIRECTION ( 'NONE',  ( 1.000000000000000000, 0.000000000000000000, 0.000000000000000000 ) ) ;
#8280=AXIS2_PLACEMENT_3D ( 'NONE', #61634, #60951, #3251 ) ;
#8285=VERTEX_POINT ( 'NONE', #31163 ) ;
#8552=VERTEX_POINT ( 'NONE', #4394 ) ;
#8565=DIRECTION ( 'NONE',  ( 0.000000000000000000, -1.000000000000000000, 0.000000000000000000 ) ) ;
#8598=ORIENTED_EDGE ( 'NONE', *, *, #15016, .F. ) ;
#8712=SURFACE_SIDE_STYLE ('',( #30385 ) ) ;
#8717=PLANE ( 'NONE',  #52064 ) ;
#8850=DIRECTION ( 'NONE',  ( 0.000000000000000000, 0.000000000000000000, -1.000000000000000000 ) ) ;
#8866=CARTESIAN_POINT ( 'NONE',  ( 5.000000000000000000, -1.199999999999999956, 9.776630298829998011 ) ) ;
#8882=ADVANCED_FACE ( 'NONE', ( #2356 ), #43635, .F. ) ;
#8921=EDGE_LOOP ( 'NONE', ( #34562, #9256, #12423, #4733, #23007 ) ) ;
#8926=DIRECTION ( 'NONE',  ( 0.9999999999999998890, -1.106867307615999853E-09, -9.864841365411998611E-09 ) ) ;
#8937=ORIENTED_EDGE ( 'NONE', *, *, #3851, .F. ) ;
#8957=DIRECTION ( 'NONE',  ( 0.000000000000000000, -1.000000000000000000, 0.000000000000000000 ) ) ;
#9045=( LENGTH_UNIT ( ) NAMED_UNIT ( * ) SI_UNIT ( .MILLI., .METRE. ) );
#9050=FACE_OUTER_BOUND ( 'NONE', #34352, .T. ) ;
#9111=DIRECTION ( 'NONE',  ( 1.000000000000000000, 0.000000000000000000, 0.000000000000000000 ) ) ;
#9201=EDGE_LOOP ( 'NONE', ( #35788, #61805, #59490, #66780 ) ) ;
#9254=DIRECTION ( 'NONE',  ( 1.000000000000000000, 3.572267238224000438E-11, -8.761989184571999838E-10 ) ) ;
#9255=LINE ( 'NONE', #45655, #60667 ) ;
#9256=ORIENTED_EDGE ( 'NONE', *, *, #18810, .T. ) ;
#9278=AXIS2_PLACEMENT_3D ( 'NONE', #30120, #9111, #41619 ) ;
#9282=LINE ( 'NONE', #14551, #49762 ) ;
#9342=CIRCLE ( 'NONE', #12708, 0.5499999999999998224 ) ;
#9362=ORIENTED_EDGE ( 'NONE', *, *, #30925, .F. ) ;
#9373=ADVANCED_FACE ( 'NONE', ( #28746, #778 ), #64733, .F. ) ;
#9380=FILL_AREA_STYLE_COLOUR ( '', #26226 ) ;
#9416=LINE ( 'NONE', #9763, #11801 ) ;
#9464=EDGE_LOOP ( 'NONE', ( #13688, #27267, #42855, #341, #48566, #1429 ) ) ;
#9467=DIRECTION ( 'NONE',  ( 0.000000000000000000, -0.7071067811865474617, -0.7071067811865474617 ) ) ;
#9512=CARTESIAN_POINT ( 'NONE',  ( 5.000000004630999584, 0.6153846187707999738, -2.423076926994999880 ) ) ;
#9564=EDGE_CURVE ( 'NONE', #31683, #34006, #58937, .T. ) ;
#9635=VECTOR ( 'NONE', #40658, 1000.000000000000114 ) ;
#9676=AXIS2_PLACEMENT_3D ( 'NONE', #40345, #19020, #18341 ) ;
#9689=ADVANCED_FACE ( 'NONE', ( #19535 ), #34402, .T. ) ;
#9723=ORIENTED_EDGE ( 'NONE', *, *, #61622, .F. ) ;
#9737=VECTOR ( 'NONE', #34873, 1000.000000000000114 ) ;
#9745=CIRCLE ( 'NONE', #48830, 1.449999999999999956 ) ;
#9763=CARTESIAN_POINT ( 'NONE',  ( 4.999999999765999625, 0.04999999976595000117, -9.776630293088999224 ) ) ;
#9826=ORIENTED_EDGE ( 'NONE', *, *, #40923, .F. ) ;
#9953=CARTESIAN_POINT ( 'NONE',  ( 7.000000000000000000, 0.000000000000000000, 0.000000000000000000 ) ) ;
#10110=VECTOR ( 'NONE', #57146, 1000.000000000000114 ) ;
#10111=B_SPLINE_CURVE_WITH_KNOTS ( 'NONE', 3,
 ( #50400, #29439, #23824, #40254 ),
 .UNSPECIFIED., .F., .F.,
 ( 4, 4 ),
 ( 0.000000000000000000, 1.000000000000000000 ),
 .UNSPECIFIED. ) ;
#10129=LINE ( 'NONE', #35678, #13946 ) ;
#10167=ORIENTED_EDGE ( 'NONE', *, *, #63027, .F. ) ;
#10216=LINE ( 'NONE', #68587, #69193 ) ;
#10269=EDGE_CURVE ( 'NONE', #30037, #46374, #15914, .T. ) ;
#10415=EDGE_CURVE ( 'NONE', #56969, #8552, #51472, .T. ) ;
#10449=AXIS2_PLACEMENT_3D ( 'NONE', #50579, #23657, #61069 ) ;
#10523=EDGE_CURVE ( 'NONE', #49128, #4545, #53506, .T. ) ;
#10531=CARTESIAN_POINT ( 'NONE',  ( 4.999999999906999726, -1.352284263165000056, 11.01731942304999912 ) ) ;
#10559=EDGE_CURVE ( 'NONE', #43884, #68795, #68192, .T. ) ;
#10610=FACE_OUTER_BOUND ( 'NONE', #6385, .T. ) ;
#10626=AXIS2_PLACEMENT_3D ( 'NONE', #28871, #17322, #33412 ) ;
#10750=CYLINDRICAL_SURFACE ( 'NONE', #41698, 2.200000000000000178 ) ;
#10768=DIRECTION ( 'NONE',  ( 1.000000000000000000, 0.000000000000000000, 0.000000000000000000 ) ) ;
#10795=AXIS2_PLACEMENT_3D ( 'NONE', #59299, #48131, #64193 ) ;
#10796=DIRECTION ( 'NONE',  ( 1.000000000000000000, 0.000000000000000000, 0.000000000000000000 ) ) ;
#10810=EDGE_CURVE ( 'NONE', #65610, #21934, #30057, .T. ) ;
#10857=ORIENTED_EDGE ( 'NONE', *, *, #35469, .T. ) ;
#10881=AXIS2_PLACEMENT_3D ( 'NONE', #51161, #30866, #25617 ) ;
#10945=AXIS2_PLACEMENT_3D ( 'NONE', #24060, #51655, #2735 ) ;
#11004=ORIENTED_EDGE ( 'NONE', *, *, #49476, .T. ) ;
#11068=CARTESIAN_POINT ( 'NONE',  ( 7.000000000000000000, 3.640000000000000124, 3.000000000000000000 ) ) ;
#11081=CARTESIAN_POINT ( 'NONE',  ( 7.000000000000000000, 0.8000000000000000444, 3.149999999999999911 ) ) ;
#11139=EDGE_CURVE ( 'NONE', #65047, #52012, #43413, .T. ) ;
#11166=VERTEX_POINT ( 'NONE', #20569 ) ;
#11225=EDGE_CURVE ( 'NONE', #37496, #18320, #38021, .T. ) ;
#11231=CARTESIAN_POINT ( 'NONE',  ( 10.90000000000000036, 0.000000000000000000, 0.000000000000000000 ) ) ;
#11294=DIRECTION ( 'NONE',  ( 0.000000000000000000, 0.7071067811865474617, -0.7071067811865474617 ) ) ;
#11304=CLOSED_SHELL ( 'NONE', ( #30664, #35530, #45843, #30413, #59739, #52642, #56751, #64994, #41660, #7142, #20661, #44056, #66437, #53177, #51603, #22660, #31494, #41217, #14928, #13149, #3222, #8882, #50046, #21767, #39085, #59095, #55794, #58612, #45783, #51240, #26319, #26919, #54887, #11906, #11613, #58645, #26349, #40703, #22388, #7171, #9689, #9373 ) ) ;
#11498=DIRECTION ( 'NONE',  ( -1.000000000000000000, 0.000000000000000000, 0.000000000000000000 ) ) ;
#11558=ORIENTED_EDGE ( 'NONE', *, *, #38918, .T. ) ;
#11596=AXIS2_PLACEMENT_3D ( 'NONE', #52991, #17216, #22110 ) ;
#11613=ADVANCED_FACE ( 'NONE', ( #21176 ), #25541, .F. ) ;
#11632=CARTESIAN_POINT ( 'NONE',  ( 7.000000000000000000, -11.29999999999999893, 0.000000000000000000 ) ) ;
#11670=CYLINDRICAL_SURFACE ( 'NONE', #6898, 10.80000000000000071 ) ;
#11730=EDGE_CURVE ( 'NONE', #24513, #62590, #57535, .T. ) ;
#11801=VECTOR ( 'NONE', #19582, 1000.000000000000114 ) ;
#11802=CARTESIAN_POINT ( 'NONE',  ( 10.90000000000000036, -1.199999999999999956, -9.776630298829998011 ) ) ;
#11879=AXIS2_PLACEMENT_3D ( 'NONE', #32425, #53740, #63179 ) ;
#11906=ADVANCED_FACE ( 'NONE', ( #7503 ), #60649, .T. ) ;
#12036=FACE_OUTER_BOUND ( 'NONE', #61477, .T. ) ;
#12053=EDGE_LOOP ( 'NONE', ( #10857, #28681, #44984 ) ) ;
#12074=ORIENTED_EDGE ( 'NONE', *, *, #25835, .F. ) ;
#12259=VERTEX_POINT ( 'NONE', #56790 ) ;
#12272=CARTESIAN_POINT ( 'NONE',  ( 7.000000000000000000, 0.5415384615382000666, 2.132307692307999769 ) ) ;
#12314=CARTESIAN_POINT ( 'NONE',  ( 5.000000000000000000, 0.05000000000000000278, -9.776630298829998011 ) ) ;
#12346=CARTESIAN_POINT ( 'NONE',  ( 10.90000000000000036, -8.618205959414002137, -7.308661029293999967 ) ) ;
#12423=ORIENTED_EDGE ( 'NONE', *, *, #31740, .T. ) ;
#12554=ORIENTED_EDGE ( 'NONE', *, *, #16578, .T. ) ;
#12562=CIRCLE ( 'NONE', #44961, 1.600000000000000089 ) ;
#12583=DIRECTION ( 'NONE',  ( 0.000000000000000000, 0.000000000000000000, -1.000000000000000000 ) ) ;
#12607=PLANE ( 'NONE',  #38286 ) ;
#12647=DIRECTION ( 'NONE',  ( 1.000000000000000000, 0.000000000000000000, 0.000000000000000000 ) ) ;
#12708=AXIS2_PLACEMENT_3D ( 'NONE', #11081, #58628, #63862 ) ;
#12713=AXIS2_PLACEMENT_3D ( 'NONE', #13381, #8123, #45535 ) ;
#12733=ORIENTED_EDGE ( 'NONE', *, *, #57227, .F. ) ;
#12769=AXIS2_PLACEMENT_3D ( 'NONE', #33370, #54685, #33718 ) ;
#12783=ORIENTED_EDGE ( 'NONE', *, *, #61091, .T. ) ;
#12784=FACE_OUTER_BOUND ( 'NONE', #8921, .T. ) ;
#12847=CARTESIAN_POINT ( 'NONE',  ( 7.169256274120943573, 0.2499999999999997224, -3.082564036157278586 ) ) ;
#12985=ORIENTED_EDGE ( 'NONE', *, *, #37473, .T. ) ;
#13046=CARTESIAN_POINT ( 'NONE',  ( 8.281163468719425325, -9.408291950837329054, -6.292115732828485797 ) ) ;
#13149=ADVANCED_FACE ( 'NONE', ( #58714 ), #19896, .F. ) ;
#13169=PRESENTATION_STYLE_ASSIGNMENT (( #55461 ) ) ;
#13205=VECTOR ( 'NONE', #2135, 999.9999999999998863 ) ;
#13356=CARTESIAN_POINT ( 'NONE',  ( 10.90000000000000036, -8.263403946409999534, -6.953859016290999229 ) ) ;
#13381=CARTESIAN_POINT ( 'NONE',  ( 5.200000000000000178, -1.199999999999999956, -9.776630298829998011 ) ) ;
#13464=AXIS2_PLACEMENT_3D ( 'NONE', #16527, #21091, #36830 ) ;
#13486=EDGE_LOOP ( 'NONE', ( #60676, #38256, #12733, #55704 ) ) ;
#13541=EDGE_LOOP ( 'NONE', ( #53020, #68405, #8598, #54103, #41563, #59655, #11004, #19528 ) ) ;
#13623=ORIENTED_EDGE ( 'NONE', *, *, #35828, .T. ) ;
#13624=VERTEX_POINT ( 'NONE', #28200 ) ;
#13677=AXIS2_PLACEMENT_3D ( 'NONE', #22029, #59098, #27638 ) ;
#13688=ORIENTED_EDGE ( 'NONE', *, *, #39332, .F. ) ;
#13715=ORIENTED_EDGE ( 'NONE', *, *, #6686, .T. ) ;
#13830=DIRECTION ( 'NONE',  ( 0.000000000000000000, 0.000000000000000000, -1.000000000000000000 ) ) ;
#13888=ORIENTED_EDGE ( 'NONE', *, *, #26214, .T. ) ;
#13946=VECTOR ( 'NONE', #52779, 1000.000000000000000 ) ;
#13967=AXIS2_PLACEMENT_3D ( 'NONE', #2290, #2630, #56113 ) ;
#13989=CARTESIAN_POINT ( 'NONE',  ( 7.307500000000000107, 0.2500000000000000000, 3.149999999999999911 ) ) ;
#13996=VERTEX_POINT ( 'NONE', #31902 ) ;
#14004=CARTESIAN_POINT ( 'NONE',  ( 8.060840674114750470, -9.103590313266890277, 5.835422151730303320 ) ) ;
#14179=ORIENTED_EDGE ( 'NONE', *, *, #20126, .T. ) ;
#14301=VECTOR ( 'NONE', #32047, 1000.000000000000000 ) ;
#14358=VERTEX_POINT ( 'NONE', #33811 ) ;
#14439=DIRECTION ( 'NONE',  ( 1.000000000000000000, 0.000000000000000000, 0.000000000000000000 ) ) ;
#14442=DIRECTION ( 'NONE',  ( -0.8987684456439055669, 0.000000000000000000, 0.4384236320214022764 ) ) ;
#14551=CARTESIAN_POINT ( 'NONE',  ( 10.90000000000000036, -8.263403946409999534, -6.953859016290999229 ) ) ;
#14646=DIRECTION ( 'NONE',  ( 0.000000000000000000, -0.2461538461538895772, 0.9692307692307582379 ) ) ;
#14647=CARTESIAN_POINT ( 'NONE',  ( 10.90000000000000036, -1.315736040608999957, -10.71955403322999878 ) ) ;
#14764=VECTOR ( 'NONE', #199, 1000.000000000000114 ) ;
#14839=ORIENTED_EDGE ( 'NONE', *, *, #31021, .F. ) ;
#14848=CARTESIAN_POINT ( 'NONE',  ( 5.000000001445999764, 1.799999998554000058, -4.283815592157999860E-09 ) ) ;
#14881=EDGE_LOOP ( 'NONE', ( #48197, #8170, #4106, #1723, #9826 ) ) ;
#14899=EDGE_LOOP ( 'NONE', ( #6304, #60484, #52994, #42147, #60597 ) ) ;
#14904=DIRECTION ( 'NONE',  ( -1.000000000000000000, 0.000000000000000000, 0.000000000000000000 ) ) ;
#14928=ADVANCED_FACE ( 'NONE', ( #61500 ), #49629, .F. ) ;
#14957=EDGE_CURVE ( 'NONE', #65610, #37496, #39925, .T. ) ;
#14963=CARTESIAN_POINT ( 'NONE',  ( 7.000000000000000000, 0.2708497377871000311, 3.000000000000000000 ) ) ;
#14984=FACE_BOUND ( 'NONE', #29924, .T. ) ;
#15016=EDGE_CURVE ( 'NONE', #32203, #64186, #33823, .T. ) ;
#15222=LINE ( 'NONE', #36547, #6110 ) ;
#15255=ORIENTED_EDGE ( 'NONE', *, *, #63339, .T. ) ;
#15265=EDGE_CURVE ( 'NONE', #43864, #62706, #36562, .T. ) ;
#15278=AXIS2_PLACEMENT_3D ( 'NONE', #57872, #26058, #47387 ) ;
#15297=CARTESIAN_POINT ( 'NONE',  ( 7.204898016025000018, -0.2500000000000000000, -3.099950251719000072 ) ) ;
#15327=ORIENTED_EDGE ( 'NONE', *, *, #15016, .T. ) ;
#15396=EDGE_CURVE ( 'NONE', #36962, #64274, #4217, .T. ) ;
#15400=AXIS2_PLACEMENT_3D ( 'NONE', #62148, #55882, #50290 ) ;
#15546=CARTESIAN_POINT ( 'NONE',  ( 5.200000000000000178, -1.376649746192999846, -11.21582968292000082 ) ) ;
#15567=EDGE_LOOP ( 'NONE', ( #61818, #30775, #47169, #3101, #37045 ) ) ;
#15599=CARTESIAN_POINT ( 'NONE',  ( 5.000000000000000000, 1.800000000000000044, 0.000000000000000000 ) ) ;
#15651=EDGE_LOOP ( 'NONE', ( #62014, #25194, #45476, #20957 ) ) ;
#15836=CYLINDRICAL_SURFACE ( 'NONE', #13464, 0.9499999999999999556 ) ;
#15914=LINE ( 'NONE', #5768, #36953 ) ;
#15995=FACE_OUTER_BOUND ( 'NONE', #47456, .T. ) ;
#15998=EDGE_CURVE ( 'NONE', #14358, #56969, #59117, .T. ) ;
#16018=EDGE_LOOP ( 'NONE', ( #10167, #12074, #12554, #13888, #60911 ) ) ;
#16123=DIRECTION ( 'NONE',  ( 1.000000000000000000, 0.000000000000000000, 0.000000000000000000 ) ) ;
#16134=EDGE_CURVE ( 'NONE', #23202, #21742, #31630, .T. ) ;
#16342=CARTESIAN_POINT ( 'NONE',  ( 5.500000000000000000, 0.000000000000000000, 0.000000000000000000 ) ) ;
#16383=DIRECTION ( 'NONE',  ( 0.000000000000000000, -1.000000000000000000, 0.000000000000000000 ) ) ;
#16471=EDGE_CURVE ( 'NONE', #65069, #57137, #10216, .T. ) ;
#16527=CARTESIAN_POINT ( 'NONE',  ( 5.500000000000000000, -1.199999999999999956, -9.776630298829998011 ) ) ;
#16539=AXIS2_PLACEMENT_3D ( 'NONE', #48226, #11498, #58034 ) ;
#16578=EDGE_CURVE ( 'NONE', #12259, #69104, #32331, .T. ) ;
#16605=DIRECTION ( 'NONE',  ( 0.000000000000000000, 0.000000000000000000, -1.000000000000000000 ) ) ;
#16624=AXIS2_PLACEMENT_3D ( 'NONE', #63233, #41582, #3820 ) ;
#16705=DIRECTION ( 'NONE',  ( 1.000000000000000000, 0.000000000000000000, 0.000000000000000000 ) ) ;
#16755=ORIENTED_EDGE ( 'NONE', *, *, #20126, .F. ) ;
#16778=CARTESIAN_POINT ( 'NONE',  ( 10.90000000000000036, 0.2500000000000000000, -4.902439024389999567 ) ) ;
#16859=CARTESIAN_POINT ( 'NONE',  ( 5.200000000000000178, 0.2500000000000000000, -9.776630298829998011 ) ) ;
#16920=VERTEX_POINT ( 'NONE', #34663 ) ;
#16924=VERTEX_POINT ( 'NONE', #18577 ) ;
#17029=CARTESIAN_POINT ( 'NONE',  ( 7.000000000000000000, -0.2392304845412999981, 3.000000000000000000 ) ) ;
#17067=CIRCLE ( 'NONE', #55012, 1.800000000000000044 ) ;
#17085=CIRCLE ( 'NONE', #36063, 0.7500000000000000000 ) ;
#17093=VECTOR ( 'NONE', #12583, 1000.000000000000000 ) ;
#17122=AXIS2_PLACEMENT_3D ( 'NONE', #41917, #42608, #63226 ) ;
#17216=DIRECTION ( 'NONE',  ( -1.000000000000000000, 0.000000000000000000, 0.000000000000000000 ) ) ;
#17226=AXIS2_PLACEMENT_3D ( 'NONE', #65559, #61015, #17682 ) ;
#17230=CYLINDRICAL_SURFACE ( 'NONE', #38042, 0.9499999999999999556 ) ;
#17322=DIRECTION ( 'NONE',  ( -1.000000000000000000, 0.000000000000000000, 0.000000000000000000 ) ) ;
#17359=CARTESIAN_POINT ( 'NONE',  ( 10.90000000000000036, -1.199999999999999956, -9.776630298829998011 ) ) ;
#17369=CARTESIAN_POINT ( 'NONE',  ( 5.000000000000000000, 0.8000000000000000444, 3.149999999999999911 ) ) ;
#17384=CARTESIAN_POINT ( 'NONE',  ( 7.102397164862999546, -0.2464401224313000349, 3.049949836518000001 ) ) ;
#17479=ORIENTED_EDGE ( 'NONE', *, *, #52310, .F. ) ;
#17538=VECTOR ( 'NONE', #22848, 1000.000000000000114 ) ;
#17637=EDGE_CURVE ( 'NONE', #38378, #31683, #10111, .T. ) ;
#17638=DIRECTION ( 'NONE',  ( 1.000000000000000000, 0.000000000000000000, 0.000000000000000000 ) ) ;
#17653=VERTEX_POINT ( 'NONE', #29785 ) ;
#17682=DIRECTION ( 'NONE',  ( 0.000000000000000000, -0.1218274111675001353, -0.9925512993736016476 ) ) ;
#17716=EDGE_LOOP ( 'NONE', ( #48417, #48142, #29612, #14839 ) ) ;
#17898=CARTESIAN_POINT ( 'NONE',  ( 5.500000000000000000, 0.8000000000000000444, -3.149999999999999911 ) ) ;
#17935=CARTESIAN_POINT ( 'NONE',  ( 10.90000000000000036, -1.199999999999999956, 9.776630298829998011 ) ) ;
#17958=VECTOR ( 'NONE', #11294, 1000.000000000000114 ) ;
#17980=ORIENTED_EDGE ( 'NONE', *, *, #3689, .T. ) ;
#18029=DIRECTION ( 'NONE',  ( -0.7071067811865475727, 0.7071067811865475727, 0.000000000000000000 ) ) ;
#18046=PLANE ( 'NONE',  #63290 ) ;
#18165=CARTESIAN_POINT ( 'NONE',  ( 7.000000000000000000, 0.000000000000000000, 0.000000000000000000 ) ) ;
#18204=ORIENTED_EDGE ( 'NONE', *, *, #40469, .F. ) ;
#18244=CARTESIAN_POINT ( 'NONE',  ( 5.500000000000000000, 2.200000000000000178, 0.000000000000000000 ) ) ;
#18281=DIRECTION ( 'NONE',  ( -0.000000000000000000, 1.000000000000000000, 0.000000000000000000 ) ) ;
#18320=VERTEX_POINT ( 'NONE', #51343 ) ;
#18324=PLANE ( 'NONE',  #19447 ) ;
#18341=DIRECTION ( 'NONE',  ( 1.000000000000000000, 0.000000000000000000, 0.000000000000000000 ) ) ;
#18345=DIRECTION ( 'NONE',  ( 0.000000000000000000, -1.000000000000000000, 0.000000000000000000 ) ) ;
#18380=ORIENTED_EDGE ( 'NONE', *, *, #10415, .T. ) ;
#18386=AXIS2_PLACEMENT_3D ( 'NONE', #5737, #58198, #5053 ) ;
#18479=EDGE_CURVE ( 'NONE', #54437, #8552, #58520, .T. ) ;
#18539=EDGE_CURVE ( 'NONE', #3659, #24513, #26844, .T. ) ;
#18577=CARTESIAN_POINT ( 'NONE',  ( 5.000000000000000000, 0.6153846153845999867, 2.423076923076999734 ) ) ;
#18590=DIRECTION ( 'NONE',  ( 1.000000000000000000, 0.000000000000000000, 0.000000000000000000 ) ) ;
#18596=CARTESIAN_POINT ( 'NONE',  ( 9.360840674114760063, -8.748618759363480990, -6.377268954453227501 ) ) ;
#18635=VECTOR ( 'NONE', #36546, 1000.000000000000000 ) ;
#18662=ORIENTED_EDGE ( 'NONE', *, *, #51000, .T. ) ;
#18686=CARTESIAN_POINT ( 'NONE',  ( 5.200000000000000178, 0.000000000000000000, 0.000000000000000000 ) ) ;
#18695=DIRECTION ( 'NONE',  ( -0.7071067811865475727, 0.7071067811865475727, 0.000000000000000000 ) ) ;
#18707=EDGE_CURVE ( 'NONE', #31683, #64075, #60238, .T. ) ;
#18749=VERTEX_POINT ( 'NONE', #48712 ) ;
#18810=EDGE_CURVE ( 'NONE', #21934, #16920, #24626, .T. ) ;
#18840=CIRCLE ( 'NONE', #27768, 2.700000000000000178 ) ;
#18933=CARTESIAN_POINT ( 'NONE',  ( 5.500000000000000000, -0.2500000000000000000, -9.776630298829998011 ) ) ;
#18987=DIRECTION ( 'NONE',  ( 0.000000000000000000, -0.1218274111675001492, 0.9925512993736016476 ) ) ;
#19020=DIRECTION ( 'NONE',  ( 0.000000000000000000, 0.000000000000000000, 1.000000000000000000 ) ) ;
#19049=CYLINDRICAL_SURFACE ( 'NONE', #54820, 0.5500000000000000444 ) ;
#19164=CARTESIAN_POINT ( 'NONE',  ( 7.307500000000000107, -0.2500000000000000000, -3.149999999999999911 ) ) ;
#19339=CARTESIAN_POINT ( 'NONE',  ( 9.050000000000000711, -7.679126935408000065, -5.093340497782000043 ) ) ;
#19359=ORIENTED_EDGE ( 'NONE', *, *, #20910, .F. ) ;
#19375=CIRCLE ( 'NONE', #17122, 1.449999999999999956 ) ;
#19428=DIRECTION ( 'NONE',  ( 0.000000000000000000, 0.7071067811864980568, -0.7071067811865969777 ) ) ;
#19447=AXIS2_PLACEMENT_3D ( 'NONE', #2920, #17638, #65510 ) ;
#19473=CIRCLE ( 'NONE', #17226, 11.30000000000000604 ) ;
#19528=ORIENTED_EDGE ( 'NONE', *, *, #24080, .T. ) ;
#19535=FACE_OUTER_BOUND ( 'NONE', #41981, .T. ) ;
#19546=( NAMED_UNIT ( * ) PLANE_ANGLE_UNIT ( ) SI_UNIT ( $, .RADIAN. ) );
#19582=DIRECTION ( 'NONE',  ( 0.7071067811865474617, 0.7071067811865474617, -2.638502694198172937E-09 ) ) ;
#19692=DIRECTION ( 'NONE',  ( -0.8231338744408063235, -0.5678473604306591982, 0.000000000000000000 ) ) ;
#19704=DIRECTION ( 'NONE',  ( 0.000000000000000000, -1.000000000000000000, 0.000000000000000000 ) ) ;
#19740=CARTESIAN_POINT ( 'NONE',  ( 10.90000000000000036, 0.000000000000000000, 0.000000000000000000 ) ) ;
#19747=B_SPLINE_CURVE_WITH_KNOTS ( 'NONE', 3,
 ( #53425, #21594, #12847, #55145 ),
 .UNSPECIFIED., .F., .F.,
 ( 4, 4 ),
 ( 0.000000000000000000, 1.000000000000000000 ),
 .UNSPECIFIED. ) ;
#19765=PRODUCT_CONTEXT ( 'NONE', #65948, 'mechanical' ) ;
#19878=CARTESIAN_POINT ( 'NONE',  ( 5.500000000000000000, 0.000000000000000000, 0.000000000000000000 ) ) ;
#19896=CONICAL_SURFACE ( 'NONE', #16539, 1.699999998954999869, 0.7853981633972997312 ) ;
#19923=UNCERTAINTY_MEASURE_WITH_UNIT (LENGTH_MEASURE( 1.000000000000000082E-05 ), #46116, 'distance_accuracy_value', 'NONE');
#20126=EDGE_CURVE ( 'NONE', #13996, #43864, #49176, .T. ) ;
#20223=ORIENTED_EDGE ( 'NONE', *, *, #15265, .F. ) ;
#20286=VECTOR ( 'NONE', #22455, 1000.000000000000000 ) ;
#20313=EDGE_CURVE ( 'NONE', #43884, #55241, #63043, .T. ) ;
#20333=DIRECTION ( 'NONE',  ( 0.7071067811866525998, 0.000000000000000000, -0.7071067811864425456 ) ) ;
#20399=FACE_OUTER_BOUND ( 'NONE', #39655, .T. ) ;
#20488=CIRCLE ( 'NONE', #10449, 11.30000000000000604 ) ;
#20509=DIRECTION ( 'NONE',  ( 0.000000000000000000, -1.000000000000000000, 0.000000000000000000 ) ) ;
#20516=CARTESIAN_POINT ( 'NONE',  ( 7.307500000000000107, -0.2500000000000000000, -3.149999999999999911 ) ) ;
#20537=CARTESIAN_POINT ( 'NONE',  ( 7.000000000000000000, -9.735955015381000166, 5.735955015381000166 ) ) ;
#20569=CARTESIAN_POINT ( 'NONE',  ( 10.90000000000000036, -0.2500000000000000000, 4.902439024389999567 ) ) ;
#20623=DIRECTION ( 'NONE',  ( 1.000000000000000000, 0.000000000000000000, 0.000000000000000000 ) ) ;
#20661=ADVANCED_FACE ( 'NONE', ( #20399 ), #15836, .F. ) ;
#20829=EDGE_LOOP ( 'NONE', ( #64920, #54770, #39761, #69148, #7589 ) ) ;
#20835=CARTESIAN_POINT ( 'NONE',  ( 5.100000004521000108, 0.8000000000000000444, -3.149999999999999911 ) ) ;
#20867=ORIENTED_EDGE ( 'NONE', *, *, #65103, .F. ) ;
#20910=EDGE_CURVE ( 'NONE', #17653, #55241, #32959, .T. ) ;
#20957=ORIENTED_EDGE ( 'NONE', *, *, #29605, .F. ) ;
#21091=DIRECTION ( 'NONE',  ( 1.000000000000000000, 0.000000000000000000, 0.000000000000000000 ) ) ;
#21108=DIRECTION ( 'NONE',  ( 0.000000000000000000, 1.000000000000000000, 0.000000000000000000 ) ) ;
#21176=FACE_OUTER_BOUND ( 'NONE', #24695, .T. ) ;
#21270=CARTESIAN_POINT ( 'NONE',  ( 5.000000000000000000, 0.000000000000000000, 0.000000000000000000 ) ) ;
#21285=PLANE ( 'NONE',  #38996 ) ;
#21325=VECTOR ( 'NONE', #58065, 1000.000000000000000 ) ;
#21370=ORIENTED_EDGE ( 'NONE', *, *, #51776, .T. ) ;
#21518=DIRECTION ( 'NONE',  ( -1.000000000000000000, 0.000000000000000000, 0.000000000000000000 ) ) ;
#21537=LINE ( 'NONE', #42528, #14301 ) ;
#21594=CARTESIAN_POINT ( 'NONE',  ( 7.066756274120943537, 0.2616187012132834555, -3.032564036156816023 ) ) ;
#21597=CARTESIAN_POINT ( 'NONE',  ( 5.500000000000000000, 0.5415384615384001288, -2.132307692307999769 ) ) ;
#21678=AXIS2_PLACEMENT_3D ( 'NONE', #17359, #23299, #2656 ) ;
#21709=CIRCLE ( 'NONE', #18386, 1.049999999999999378 ) ;
#21742=VERTEX_POINT ( 'NONE', #27734 ) ;
#21760=( GEOMETRIC_REPRESENTATION_CONTEXT ( 3 ) GLOBAL_UNCERTAINTY_ASSIGNED_CONTEXT ( ( #30421 ) ) GLOBAL_UNIT_ASSIGNED_CONTEXT ( ( #9045, #52381, #67085 ) ) REPRESENTATION_CONTEXT ( 'NONE', 'WORKASPACE' ) );
#21767=ADVANCED_FACE ( 'NONE', ( #65105 ), #17230, .F. ) ;
#21790=ORIENTED_EDGE ( 'NONE', *, *, #54038, .F. ) ;
#21810=LINE ( 'NONE', #29152, #17538 ) ;
#21934=VERTEX_POINT ( 'NONE', #51119 ) ;
#22027=AXIS2_PLACEMENT_3D ( 'NONE', #66738, #50670, #7322 ) ;
#22029=CARTESIAN_POINT ( 'NONE',  ( 5.500000000000000000, 0.000000000000000000, 0.000000000000000000 ) ) ;
#22093=CARTESIAN_POINT ( 'NONE',  ( 5.000000000000000000, 0.000000000000000000, 0.000000000000000000 ) ) ;
#22110=DIRECTION ( 'NONE',  ( 0.000000000000000000, 0.000000000000000000, 1.000000000000000000 ) ) ;
#22139=CARTESIAN_POINT ( 'NONE',  ( 11.09999999999999964, 3.640000000000000124, -5.000000000000000000 ) ) ;
#22148=CARTESIAN_POINT ( 'NONE',  ( 7.000000000000000000, 2.200000000000000178, 0.000000000000000000 ) ) ;
#22155=CARTESIAN_POINT ( 'NONE',  ( 7.307500000000000107, 0.2500000000000000000, -3.149999999999999911 ) ) ;
#22158=VERTEX_POINT ( 'NONE', #32465 ) ;
#22164=DIRECTION ( 'NONE',  ( 1.000000000000000000, 0.000000000000000000, 0.000000000000000000 ) ) ;
#22372=CARTESIAN_POINT ( 'NONE',  ( 7.000000000000000000, -9.370210309074998634, 5.370210309075000410 ) ) ;
#22388=ADVANCED_FACE ( 'NONE', ( #31009 ), #25773, .T. ) ;
#22455=DIRECTION ( 'NONE',  ( -0.8987684456439055669, 0.000000000000000000, 0.4384236320214022764 ) ) ;
#22660=ADVANCED_FACE ( 'NONE', ( #12784 ), #19049, .F. ) ;
#22664=CIRCLE ( 'NONE', #53910, 11.30000000000000604 ) ;
#22848=DIRECTION ( 'NONE',  ( 0.9999999999999998890, -3.212307467389999644E-09, -9.519589316684998912E-09 ) ) ;
#22863=FACE_OUTER_BOUND ( 'NONE', #39448, .T. ) ;
#23007=ORIENTED_EDGE ( 'NONE', *, *, #14957, .F. ) ;
#23202=VERTEX_POINT ( 'NONE', #16859 ) ;
#23239=DIRECTION ( 'NONE',  ( 1.000000000000000000, 0.000000000000000000, 0.000000000000000000 ) ) ;
#23299=DIRECTION ( 'NONE',  ( -1.000000000000000000, 0.000000000000000000, 0.000000000000000000 ) ) ;
#23373=ORIENTED_EDGE ( 'NONE', *, *, #11139, .F. ) ;
#23406=DIRECTION ( 'NONE',  ( 1.000000000000000000, 0.000000000000000000, 0.000000000000000000 ) ) ;
#23509=DIRECTION ( 'NONE',  ( 1.000000000000000000, 0.000000000000000000, 0.000000000000000000 ) ) ;
#23549=CARTESIAN_POINT ( 'NONE',  ( 5.500000000000000000, 0.5415384615384001288, 2.132307692307999769 ) ) ;
#23572=ORIENTED_EDGE ( 'NONE', *, *, #30699, .T. ) ;
#23657=DIRECTION ( 'NONE',  ( -1.000000000000000000, 0.000000000000000000, 0.000000000000000000 ) ) ;
#23706=DIRECTION ( 'NONE',  ( 1.000000000000000000, -2.612724851285000276E-14, -1.006602208993000106E-14 ) ) ;
#23748=CARTESIAN_POINT ( 'NONE',  ( 7.000000000000000000, -0.2392304845412999981, -3.000000000000000000 ) ) ;
#23759=DIRECTION ( 'NONE',  ( 1.000000000000000000, -1.234748485291000148E-09, -3.354312113616000052E-09 ) ) ;
#23824=CARTESIAN_POINT ( 'NONE',  ( 8.281163468719427101, -9.408291950837330830, 6.292115732828488461 ) ) ;
#23832=EDGE_CURVE ( 'NONE', #21742, #65069, #60305, .T. ) ;
#23901=DIRECTION ( 'NONE',  ( 0.4384236320213994453, -0.6355252626312994924, 0.6355252626312996034 ) ) ;
#24060=CARTESIAN_POINT ( 'NONE',  ( 9.050000000000000711, -7.679126935408000065, 5.093340497782000043 ) ) ;
#24080=EDGE_CURVE ( 'NONE', #64075, #49128, #30326, .T. ) ;
#24083=VECTOR ( 'NONE', #16123, 1000.000000000000000 ) ;
#24135=VECTOR ( 'NONE', #52294, 1000.000000000000000 ) ;
#24303=CARTESIAN_POINT ( 'NONE',  ( 5.500000000000000000, 2.200000000000000178, 0.000000000000000000 ) ) ;
#24343=LINE ( 'NONE', #44654, #59713 ) ;
#24406=PLANE ( 'NONE',  #10945 ) ;
#24493=VERTEX_POINT ( 'NONE', #51961 ) ;
#24513=VERTEX_POINT ( 'NONE', #25397 ) ;
#24526=LINE ( 'NONE', #40601, #2856 ) ;
#24626=B_SPLINE_CURVE_WITH_KNOTS ( 'NONE', 3,
 ( #13989, #52409, #46486, #46142 ),
 .UNSPECIFIED., .F., .F.,
 ( 4, 4 ),
 ( 0.000000000000000000, 1.000000000000000000 ),
 .UNSPECIFIED. ) ;
#24655=CARTESIAN_POINT ( 'NONE',  ( 7.000000000000000000, 0.000000000000000000, 0.000000000000000000 ) ) ;
#24695=EDGE_LOOP ( 'NONE', ( #2063, #12783, #48835, #23373 ) ) ;
#24705=ORIENTED_EDGE ( 'NONE', *, *, #2140, .T. ) ;
#24805=EDGE_CURVE ( 'NONE', #11166, #24880, #46565, .T. ) ;
#24857=ORIENTED_EDGE ( 'NONE', *, *, #30699, .F. ) ;
#24880=VERTEX_POINT ( 'NONE', #24891 ) ;
#24891=CARTESIAN_POINT ( 'NONE',  ( 7.307500000000000107, -0.2500000000000000000, 3.149999999999999911 ) ) ;
#24992=DIRECTION ( 'NONE',  ( 0.000000000000000000, -0.7651299950380209269, 0.6438758348417170652 ) ) ;
#25004=DIRECTION ( 'NONE',  ( 0.000000000000000000, 1.000000000000000000, 0.000000000000000000 ) ) ;
#25039=CIRCLE ( 'NONE', #8280, 1.250000000000000666 ) ;
#25194=ORIENTED_EDGE ( 'NONE', *, *, #14957, .T. ) ;
#25228=VECTOR ( 'NONE', #42699, 1000.000000000000114 ) ;
#25247=CARTESIAN_POINT ( 'NONE',  ( 5.000000000000000000, 0.05000000000000000278, -3.149999999999999911 ) ) ;
#25397=CARTESIAN_POINT ( 'NONE',  ( 10.90000000000000036, -1.315736040608999957, 10.71955403322999878 ) ) ;
#25484=EDGE_CURVE ( 'NONE', #65047, #5290, #28099, .T. ) ;
#25541=CONICAL_SURFACE ( 'NONE', #62366, 0.6499999954788998613, 0.7853981633972997312 ) ;
#25617=DIRECTION ( 'NONE',  ( 0.000000000000000000, -1.000000000000000000, 0.000000000000000000 ) ) ;
#25726=PLANE ( 'NONE',  #11596 ) ;
#25748=B_SPLINE_CURVE_WITH_KNOTS ( 'NONE', 3,
 ( #43621, #2000, #17384, #17029 ),
 .UNSPECIFIED., .F., .F.,
 ( 4, 4 ),
 ( 0.000000000000000000, 1.000000000000000000 ),
 .UNSPECIFIED. ) ;
#25765=ORIENTED_EDGE ( 'NONE', *, *, #27668, .T. ) ;
#25773=CONICAL_SURFACE ( 'NONE', #63739, 1.349999999768000336, 0.7853981633972997312 ) ;
#25809=VECTOR ( 'NONE', #51464, 1000.000000000000000 ) ;
#25835=EDGE_CURVE ( 'NONE', #12259, #24880, #65757, .T. ) ;
#25849=CYLINDRICAL_SURFACE ( 'NONE', #50679, 11.29999999999999893 ) ;
#26051=EDGE_LOOP ( 'NONE', ( #43692, #40036, #66369, #33886, #54597 ) ) ;
#26058=DIRECTION ( 'NONE',  ( 1.000000000000000000, 0.000000000000000000, 0.000000000000000000 ) ) ;
#26100=CARTESIAN_POINT ( 'NONE',  ( 5.099999999768000336, -1.199999999999999956, 9.776630298829998011 ) ) ;
#26112=CIRCLE ( 'NONE', #41730, 1.449999999999999956 ) ;
#26121=DIRECTION ( 'NONE',  ( 1.000000000000000000, 0.000000000000000000, 0.000000000000000000 ) ) ;
#26214=EDGE_CURVE ( 'NONE', #69104, #53505, #59916, .T. ) ;
#26226=COLOUR_RGB ( '', 0.40784314, 0.44705882, 0.49803922) ;
#26252=CARTESIAN_POINT ( 'NONE',  ( 5.500000000000000000, -0.2500000000000000000, -3.149999999999999911 ) ) ;
#26315=CARTESIAN_POINT ( 'NONE',  ( 5.500000000000000000, -1.315736040608999957, -10.71955403322999878 ) ) ;
#26319=ADVANCED_FACE ( 'NONE', ( #46944 ), #61991, .T. ) ;
#26349=ADVANCED_FACE ( 'NONE', ( #35766 ), #28773, .F. ) ;
#26391=DIRECTION ( 'NONE',  ( 0.000000000000000000, 1.000000000000000000, 0.000000000000000000 ) ) ;
#26455=DIRECTION ( 'NONE',  ( 0.000000000000000000, 1.000000000000000000, 0.000000000000000000 ) ) ;
#26788=ORIENTED_EDGE ( 'NONE', *, *, #18707, .F. ) ;
#26803=DIRECTION ( 'NONE',  ( 1.000000000000000000, 0.000000000000000000, 0.000000000000000000 ) ) ;
#26844=CIRCLE ( 'NONE', #53625, 10.80000000000000249 ) ;
#26919=ADVANCED_FACE ( 'NONE', ( #62840 ), #48153, .T. ) ;
#26951=ORIENTED_EDGE ( 'NONE', *, *, #27668, .F. ) ;
#27048=DIRECTION ( 'NONE',  ( 1.000000000000000000, 0.000000000000000000, 0.000000000000000000 ) ) ;
#27138=EDGE_CURVE ( 'NONE', #64274, #52415, #59890, .T. ) ;
#27147=CARTESIAN_POINT ( 'NONE',  ( 5.500000000000000000, 0.000000000000000000, 0.000000000000000000 ) ) ;
#27229=CARTESIAN_POINT ( 'NONE',  ( 5.000000000000000000, 0.000000000000000000, 0.000000000000000000 ) ) ;
#27267=ORIENTED_EDGE ( 'NONE', *, *, #37397, .F. ) ;
#27289=CARTESIAN_POINT ( 'NONE',  ( 5.000000000000000000, 0.6153846153845999867, -2.423076923076999734 ) ) ;
#27323=DIRECTION ( 'NONE',  ( 0.000000000000000000, 0.2461538461537955691, -0.9692307692307821076 ) ) ;
#27362=ORIENTED_EDGE ( 'NONE', *, *, #50216, .T. ) ;
#27449=DIRECTION ( 'NONE',  ( 1.000000000000000000, -6.763579949425000297E-11, 5.896569782073000140E-12 ) ) ;
#27556=CIRCLE ( 'NONE', #15278, 2.199999999999999734 ) ;
#27578=ORIENTED_EDGE ( 'NONE', *, *, #54038, .T. ) ;
#27609=ORIENTED_EDGE ( 'NONE', *, *, #68170, .T. ) ;
#27628=VECTOR ( 'NONE', #23706, 1000.000000000000000 ) ;
#27638=DIRECTION ( 'NONE',  ( 0.000000000000000000, 0.2461538461537955691, -0.9692307692307821076 ) ) ;
#27664=EDGE_CURVE ( 'NONE', #64274, #42800, #36201, .T. ) ;
#27668=EDGE_CURVE ( 'NONE', #30122, #69104, #27556, .T. ) ;
#27723=CARTESIAN_POINT ( 'NONE',  ( 10.90000000000000036, -0.2500000000000000000, -4.902439024389999567 ) ) ;
#27734=CARTESIAN_POINT ( 'NONE',  ( 10.90000000000000036, 0.2500000000000000000, -9.776630298829998011 ) ) ;
#27748=PLANE ( 'NONE',  #52002 ) ;
#27768=AXIS2_PLACEMENT_3D ( 'NONE', #24655, #61374, #66611 ) ;
#27794=EDGE_CURVE ( 'NONE', #49128, #37678, #61007, .T. ) ;
#27885=DIRECTION ( 'NONE',  ( 0.000000000000000000, -0.2461538461540070666, 0.9692307692307283729 ) ) ;
#27887=DIRECTION ( 'NONE',  ( 1.000000000000000000, 0.000000000000000000, 0.000000000000000000 ) ) ;
#28099=LINE ( 'NONE', #9512, #43275 ) ;
#28129=ORIENTED_EDGE ( 'NONE', *, *, #18810, .F. ) ;
#28185=CIRCLE ( 'NONE', #67250, 2.700000000000000178 ) ;
#28200=CARTESIAN_POINT ( 'NONE',  ( 5.000000000000000000, 0.05000000000000000278, 9.776630298829998011 ) ) ;
#28340=ORIENTED_EDGE ( 'NONE', *, *, #16471, .T. ) ;
#28353=EDGE_CURVE ( 'NONE', #46383, #62706, #58315, .T. ) ;
#28361=PLANE ( 'NONE',  #7597 ) ;
#28366=DIRECTION ( 'NONE',  ( 0.7071067811865969777, 0.7071067811864980568, 3.301816515101990092E-09 ) ) ;
#28566=ORIENTED_EDGE ( 'NONE', *, *, #11225, .T. ) ;
#28570=AXIS2_PLACEMENT_3D ( 'NONE', #17898, #12647, #35017 ) ;
#28623=ORIENTED_EDGE ( 'NONE', *, *, #56998, .T. ) ;
#28651=ORIENTED_EDGE ( 'NONE', *, *, #64369, .T. ) ;
#28678=AXIS2_PLACEMENT_3D ( 'NONE', #65235, #41769, #46680 ) ;
#28681=ORIENTED_EDGE ( 'NONE', *, *, #2664, .T. ) ;
#28719=CARTESIAN_POINT ( 'NONE',  ( 5.500000000000000000, -0.2500000000000000000, 3.149999999999999911 ) ) ;
#28734=ORIENTED_EDGE ( 'NONE', *, *, #65103, .T. ) ;
#28746=FACE_BOUND ( 'NONE', #12053, .T. ) ;
#28773=CONICAL_SURFACE ( 'NONE', #67815, 0.6499999954790001144, 0.7853981633972997312 ) ;
#28782=LINE ( 'NONE', #38914, #31068 ) ;
#28871=CARTESIAN_POINT ( 'NONE',  ( 5.100000001045000175, 0.000000000000000000, 0.000000000000000000 ) ) ;
#28897=EDGE_CURVE ( 'NONE', #8552, #14358, #12562, .T. ) ;
#28932=DIRECTION ( 'NONE',  ( 1.000000000000000000, 0.000000000000000000, 0.000000000000000000 ) ) ;
#29121=PRODUCT_DEFINITION ( 'UNKNOWN', '', #35160, #62559 ) ;
#29152=CARTESIAN_POINT ( 'NONE',  ( 5.200000000963999724, -1.599999999036000098, 2.855876981774999784E-09 ) ) ;
#29216=DIRECTION ( 'NONE',  ( 1.000000000000000000, 0.000000000000000000, 0.000000000000000000 ) ) ;
#29304=ORIENTED_EDGE ( 'NONE', *, *, #65016, .T. ) ;
#29329=VECTOR ( 'NONE', #67272, 1000.000000000000000 ) ;
#29355=DIRECTION ( 'NONE',  ( 1.000000000000000000, 0.000000000000000000, 0.000000000000000000 ) ) ;
#29436=FACE_OUTER_BOUND ( 'NONE', #59575, .T. ) ;
#29439=CARTESIAN_POINT ( 'NONE',  ( 9.581163468719390508, -9.035708932181609754, 6.816351070799544054 ) ) ;
#29451=CIRCLE ( 'NONE', #42793, 2.199999999999999734 ) ;
#29605=EDGE_CURVE ( 'NONE', #48769, #16924, #17085, .T. ) ;
#29612=ORIENTED_EDGE ( 'NONE', *, *, #59258, .F. ) ;
#29681=ORIENTED_EDGE ( 'NONE', *, *, #40592, .F. ) ;
#29785=CARTESIAN_POINT ( 'NONE',  ( 10.90000000000000036, -0.2500000000000000000, -4.902439024389999567 ) ) ;
#29819=DIRECTION ( 'NONE',  ( 1.000000000000000000, 0.000000000000000000, 0.000000000000000000 ) ) ;
#29877=VECTOR ( 'NONE', #60959, 1000.000000000000000 ) ;
#29897=VERTEX_POINT ( 'NONE', #62420 ) ;
#29924=EDGE_LOOP ( 'NONE', ( #6841, #24705 ) ) ;
#30037=VERTEX_POINT ( 'NONE', #3682 ) ;
#30057=LINE ( 'NONE', #61847, #57060 ) ;
#30087=ORIENTED_EDGE ( 'NONE', *, *, #10810, .F. ) ;
#30120=CARTESIAN_POINT ( 'NONE',  ( 5.099999999983999999, -3.441691376337999159E-14, 1.598721155459999804E-14 ) ) ;
#30122=VERTEX_POINT ( 'NONE', #18244 ) ;
#30187=DIRECTION ( 'NONE',  ( -1.000000000000000000, 0.000000000000000000, 0.000000000000000000 ) ) ;
#30199=EDGE_CURVE ( 'NONE', #62414, #79, #51676, .T. ) ;
#30266=SHAPE_DEFINITION_REPRESENTATION ( #34392, #46027 ) ;
#30298=DIRECTION ( 'NONE',  ( -1.000000000000000000, 0.000000000000000000, 0.000000000000000000 ) ) ;
#30326=CIRCLE ( 'NONE', #57110, 10.79999999999999893 ) ;
#30385=SURFACE_STYLE_FILL_AREA ( #56605 ) ;
#30413=ADVANCED_FACE ( 'NONE', ( #15995 ), #10750, .F. ) ;
#30421=UNCERTAINTY_MEASURE_WITH_UNIT (LENGTH_MEASURE( 1.000000000000000082E-05 ), #9045, 'distance_accuracy_value', 'NONE');
#30526=PLANE ( 'NONE',  #35131 ) ;
#30553=DIRECTION ( 'NONE',  ( 1.000000000000000000, 0.000000000000000000, 0.000000000000000000 ) ) ;
#30577=CIRCLE ( 'NONE', #12713, 1.449999999999999956 ) ;
#30611=EDGE_CURVE ( 'NONE', #24493, #30037, #20488, .T. ) ;
#30664=ADVANCED_FACE ( 'NONE', ( #38273 ), #4856, .T. ) ;
#30699=EDGE_CURVE ( 'NONE', #43332, #53505, #29451, .T. ) ;
#30723=( NAMED_UNIT ( * ) SI_UNIT ( $, .STERADIAN. ) SOLID_ANGLE_UNIT ( ) );
#30762=ORIENTED_EDGE ( 'NONE', *, *, #3851, .T. ) ;
#30775=ORIENTED_EDGE ( 'NONE', *, *, #43758, .F. ) ;
#30826=CIRCLE ( 'NONE', #43097, 1.600000000000000089 ) ;
#30866=DIRECTION ( 'NONE',  ( 1.000000000000000000, 0.000000000000000000, 0.000000000000000000 ) ) ;
#30925=EDGE_CURVE ( 'NONE', #63702, #57137, #9255, .T. ) ;
#31009=FACE_OUTER_BOUND ( 'NONE', #3354, .T. ) ;
#31021=EDGE_CURVE ( 'NONE', #41105, #8285, #36109, .T. ) ;
#31029=ORIENTED_EDGE ( 'NONE', *, *, #24805, .T. ) ;
#31068=VECTOR ( 'NONE', #44168, 1000.000000000000000 ) ;
#31163=CARTESIAN_POINT ( 'NONE',  ( 5.500000000000000000, -1.315736040608999957, 10.71955403322999878 ) ) ;
#31494=ADVANCED_FACE ( 'NONE', ( #64192 ), #63509, .F. ) ;
#31561=ORIENTED_EDGE ( 'NONE', *, *, #56097, .F. ) ;
#31600=CARTESIAN_POINT ( 'NONE',  ( 5.500000000000000000, -0.2500000000000000000, -3.149999999999999911 ) ) ;
#31623=VECTOR ( 'NONE', #4478, 1000.000000000000000 ) ;
#31630=LINE ( 'NONE', #52950, #1085 ) ;
#31662=EDGE_LOOP ( 'NONE', ( #60783, #37893, #4131, #40832 ) ) ;
#31679=EDGE_CURVE ( 'NONE', #62706, #55241, #7550, .T. ) ;
#31683=VERTEX_POINT ( 'NONE', #20537 ) ;
#31703=DIRECTION ( 'NONE',  ( 1.000000000000000000, 0.000000000000000000, 0.000000000000000000 ) ) ;
#31716=CARTESIAN_POINT ( 'NONE',  ( 5.200000000000000178, 0.000000000000000000, 0.000000000000000000 ) ) ;
#31740=EDGE_CURVE ( 'NONE', #16920, #18320, #9342, .T. ) ;
#31743=LINE ( 'NONE', #14963, #51884 ) ;
#31875=MANIFOLD_SOLID_BREP ( 'Stock-MAS-678-1', #11304 ) ;
#31902=CARTESIAN_POINT ( 'NONE',  ( 7.000000000000000000, 0.6646153846154000400, -2.616923076922999858 ) ) ;
#32016=DIRECTION ( 'NONE',  ( 1.000000000000000000, 0.000000000000000000, 0.000000000000000000 ) ) ;
#32043=DIRECTION ( 'NONE',  ( 1.000000000000000000, 0.000000000000000000, 0.000000000000000000 ) ) ;
#32047=DIRECTION ( 'NONE',  ( 0.000000000000000000, 0.000000000000000000, -1.000000000000000000 ) ) ;
#32095=DIRECTION ( 'NONE',  ( 1.000000000000000000, 0.000000000000000000, 0.000000000000000000 ) ) ;
#32197=LINE ( 'NONE', #16778, #38359 ) ;
#32203=VERTEX_POINT ( 'NONE', #26315 ) ;
#32237=LINE ( 'NONE', #7030, #37101 ) ;
#32253=ORIENTED_EDGE ( 'NONE', *, *, #51776, .F. ) ;
#32295=ORIENTED_EDGE ( 'NONE', *, *, #41712, .F. ) ;
#32331=CIRCLE ( 'NONE', #45756, 1.050000000000000044 ) ;
#32351=ORIENTED_EDGE ( 'NONE', *, *, #31021, .T. ) ;
#32402=DIRECTION ( 'NONE',  ( -0.4384236320214023319, 0.000000000000000000, 0.8987684456439056779 ) ) ;
#32425=CARTESIAN_POINT ( 'NONE',  ( 5.000000000000000000, -1.199999999999999956, -9.776630298829998011 ) ) ;
#32465=CARTESIAN_POINT ( 'NONE',  ( 5.500000000000000000, -1.600000000000000089, 0.000000000000000000 ) ) ;
#32474=FACE_OUTER_BOUND ( 'NONE', #14881, .T. ) ;
#32792=CARTESIAN_POINT ( 'NONE',  ( 5.100000001045000175, 0.000000000000000000, -1.699999998954999869 ) ) ;
#32916=DIRECTION ( 'NONE',  ( 1.000000000000000000, 0.000000000000000000, 0.000000000000000000 ) ) ;
#32933=ORIENTED_EDGE ( 'NONE', *, *, #26214, .F. ) ;
#32959=LINE ( 'NONE', #27723, #20286 ) ;
#33009=CARTESIAN_POINT ( 'NONE',  ( 5.500000000000000000, 0.000000000000000000, 0.000000000000000000 ) ) ;
#33048=DIRECTION ( 'NONE',  ( -1.000000000000000000, 0.000000000000000000, 0.000000000000000000 ) ) ;
#33108=VECTOR ( 'NONE', #53654, 1000.000000000000000 ) ;
#33114=DIRECTION ( 'NONE',  ( -1.000000000000000000, 0.000000000000000000, 0.000000000000000000 ) ) ;
#33143=CARTESIAN_POINT ( 'NONE',  ( 5.000000000000000000, 0.000000000000000000, 0.000000000000000000 ) ) ;
#33324=DIRECTION ( 'NONE',  ( 0.000000000000000000, 1.000000000000000000, 0.000000000000000000 ) ) ;
#33355=AXIS2_PLACEMENT_3D ( 'NONE', #67701, #57218, #20509 ) ;
#33370=CARTESIAN_POINT ( 'NONE',  ( 5.099999999740999712, 0.000000000000000000, 0.000000000000000000 ) ) ;
#33383=AXIS2_PLACEMENT_3D ( 'NONE', #58317, #68109, #14646 ) ;
#33412=DIRECTION ( 'NONE',  ( 0.000000000000000000, 0.000000000000000000, -1.000000000000000000 ) ) ;
#33414=FACE_OUTER_BOUND ( 'NONE', #54045, .T. ) ;
#33490=CARTESIAN_POINT ( 'NONE',  ( 5.200000002601999682, 0.2500000026021999555, 3.150000007068999963 ) ) ;
#33631=ORIENTED_EDGE ( 'NONE', *, *, #40923, .T. ) ;
#33634=FACE_OUTER_BOUND ( 'NONE', #15567, .T. ) ;
#33718=DIRECTION ( 'NONE',  ( 0.000000000000000000, 0.000000000000000000, -1.000000000000000000 ) ) ;
#33811=CARTESIAN_POINT ( 'NONE',  ( 5.200000000000000178, -1.600000000000000089, 0.000000000000000000 ) ) ;
#33823=LINE ( 'NONE', #39405, #36563 ) ;
#33886=ORIENTED_EDGE ( 'NONE', *, *, #64761, .F. ) ;
#33938=CARTESIAN_POINT ( 'NONE',  ( 5.500000000000000000, -0.2500000000000000000, 9.776630298829998011 ) ) ;
#33982=CIRCLE ( 'NONE', #21678, 0.9499999999999999556 ) ;
#34006=VERTEX_POINT ( 'NONE', #11632 ) ;
#34022=EDGE_CURVE ( 'NONE', #38686, #46374, #6912, .T. ) ;
#34097=EDGE_CURVE ( 'NONE', #32203, #68795, #42649, .T. ) ;
#34298=CARTESIAN_POINT ( 'NONE',  ( 10.90000000000000036, -8.263403946409999534, 6.953859016290999229 ) ) ;
#34352=EDGE_LOOP ( 'NONE', ( #32351, #38020, #165, #62614, #2660, #41088, #25765, #51245, #2841 ) ) ;
#34366=CARTESIAN_POINT ( 'NONE',  ( 5.500000000000000000, -1.199999999999999956, -9.776630298829998011 ) ) ;
#34392=PRODUCT_DEFINITION_SHAPE ( 'NONE', 'NONE',  #29121 ) ;
#34402=CONICAL_SURFACE ( 'NONE', #41073, 1.349999999648999971, 0.7853981633972997312 ) ;
#34471=EDGE_LOOP ( 'NONE', ( #2775, #30762, #38084, #40489 ) ) ;
#34505=DIRECTION ( 'NONE',  ( 1.000000000000000000, 0.000000000000000000, 0.000000000000000000 ) ) ;
#34510=EDGE_LOOP ( 'NONE', ( #32253, #38779, #49007, #37749 ) ) ;
#34562=ORIENTED_EDGE ( 'NONE', *, *, #10810, .T. ) ;
#34663=CARTESIAN_POINT ( 'NONE',  ( 7.000000000000000000, 0.2708497377871000311, 3.000000000000000000 ) ) ;
#34750=EDGE_CURVE ( 'NONE', #30037, #59040, #19375, .T. ) ;
#34768=CARTESIAN_POINT ( 'NONE',  ( 5.500000000000000000, 0.5415384615384001288, 2.132307692307999769 ) ) ;
#34873=DIRECTION ( 'NONE',  ( 0.7071067811865474617, 0.7071067811865474617, -5.048527528662336139E-09 ) ) ;
#34982=AXIS2_PLACEMENT_3D ( 'NONE', #61236, #18590, #46188 ) ;
#35017=DIRECTION ( 'NONE',  ( 0.000000000000000000, 1.000000000000000000, 0.000000000000000000 ) ) ;
#35116=ORIENTED_EDGE ( 'NONE', *, *, #58305, .T. ) ;
#35131=AXIS2_PLACEMENT_3D ( 'NONE', #19339, #23901, #19692 ) ;
#35160=PRODUCT_DEFINITION_FORMATION_WITH_SPECIFIED_SOURCE ( 'ANY', '', #61183, .NOT_KNOWN. ) ;
#35208=ORIENTED_EDGE ( 'NONE', *, *, #15396, .T. ) ;
#35259=ORIENTED_EDGE ( 'NONE', *, *, #30199, .T. ) ;
#35469=EDGE_CURVE ( 'NONE', #59964, #64650, #43989, .T. ) ;
#35530=ADVANCED_FACE ( 'NONE', ( #63929 ), #25849, .T. ) ;
#35678=CARTESIAN_POINT ( 'NONE',  ( 5.000000004069000248, 0.6153845687985000090, 2.423076939105999639 ) ) ;
#35741=ORIENTED_EDGE ( 'NONE', *, *, #2357, .T. ) ;
#35766=FACE_OUTER_BOUND ( 'NONE', #15651, .T. ) ;
#35788=ORIENTED_EDGE ( 'NONE', *, *, #6686, .F. ) ;
#35815=LINE ( 'NONE', #51883, #29329 ) ;
#35828=EDGE_CURVE ( 'NONE', #79, #21742, #26112, .T. ) ;
#35893=LINE ( 'NONE', #46736, #9737 ) ;
#35905=VERTEX_POINT ( 'NONE', #21597 ) ;
#36063=AXIS2_PLACEMENT_3D ( 'NONE', #17369, #34505, #60366 ) ;
#36065=B_SPLINE_CURVE_WITH_KNOTS ( 'NONE', 3,
 ( #34298, #55621, #14004, #7720 ),
 .UNSPECIFIED., .F., .F.,
 ( 4, 4 ),
 ( 0.000000000000000000, 1.000000000000000000 ),
 .UNSPECIFIED. ) ;
#36109=CIRCLE ( 'NONE', #36158, 0.9499999999999999556 ) ;
#36140=CARTESIAN_POINT ( 'NONE',  ( 7.000000000000000000, 0.000000000000000000, 0.000000000000000000 ) ) ;
#36158=AXIS2_PLACEMENT_3D ( 'NONE', #50893, #61383, #25004 ) ;
#36170=CARTESIAN_POINT ( 'NONE',  ( 10.90000000000000036, 0.000000000000000000, 0.000000000000000000 ) ) ;
#36201=LINE ( 'NONE', #52280, #18635 ) ;
#36218=DIRECTION ( 'NONE',  ( 0.000000000000000000, 1.000000000000000000, 0.000000000000000000 ) ) ;
#36492=CIRCLE ( 'NONE', #40945, 11.29999999999999538 ) ;
#36546=DIRECTION ( 'NONE',  ( 0.7071067811865093811, -0.08614499102994124802, -0.7018397541608093482 ) ) ;
#36547=CARTESIAN_POINT ( 'NONE',  ( 10.90000000000000036, 0.2500000000000000000, 9.776630298829998011 ) ) ;
#36562=LINE ( 'NONE', #52295, #49995 ) ;
#36563=VECTOR ( 'NONE', #27887, 1000.000000000000000 ) ;
#36594=AXIS2_PLACEMENT_3D ( 'NONE', #58601, #26803, #5799 ) ;
#36620=ORIENTED_EDGE ( 'NONE', *, *, #37397, .T. ) ;
#36659=CARTESIAN_POINT ( 'NONE',  ( 5.500000000000000000, -0.2500000000000000000, 9.776630298829998011 ) ) ;
#36779=CARTESIAN_POINT ( 'NONE',  ( 7.000000000000000000, -9.370210309074998634, -5.370210309075000410 ) ) ;
#36830=DIRECTION ( 'NONE',  ( 0.000000000000000000, 1.000000000000000000, 0.000000000000000000 ) ) ;
#36924=CARTESIAN_POINT ( 'NONE',  ( 5.200000000000000178, 0.000000000000000000, 0.000000000000000000 ) ) ;
#36953=VECTOR ( 'NONE', #27449, 1000.000000000000000 ) ;
#36962=VERTEX_POINT ( 'NONE', #41149 ) ;
#37004=LINE ( 'NONE', #32792, #5297 ) ;
#37045=ORIENTED_EDGE ( 'NONE', *, *, #31679, .F. ) ;
#37101=VECTOR ( 'NONE', #28366, 1000.000000000000000 ) ;
#37249=LINE ( 'NONE', #41466, #24135 ) ;
#37312=ORIENTED_EDGE ( 'NONE', *, *, #15998, .T. ) ;
#37350=DIRECTION ( 'NONE',  ( 1.000000000000000000, 0.000000000000000000, 0.000000000000000000 ) ) ;
#37390=ORIENTED_EDGE ( 'NONE', *, *, #59428, .F. ) ;
#37397=EDGE_CURVE ( 'NONE', #42800, #24493, #19473, .T. ) ;
#37424=CARTESIAN_POINT ( 'NONE',  ( 10.90000000000000036, 0.2500000000000000000, -4.902439024389999567 ) ) ;
#37473=EDGE_CURVE ( 'NONE', #64186, #37678, #65225, .T. ) ;
#37496=VERTEX_POINT ( 'NONE', #66936 ) ;
#37543=ORIENTED_EDGE ( 'NONE', *, *, #51522, .T. ) ;
#37678=VERTEX_POINT ( 'NONE', #49398 ) ;
#37701=EDGE_CURVE ( 'NONE', #4545, #62414, #68020, .T. ) ;
#37749=ORIENTED_EDGE ( 'NONE', *, *, #40469, .T. ) ;
#37835=DIRECTION ( 'NONE',  ( 1.000000000000000000, 0.000000000000000000, 0.000000000000000000 ) ) ;
#37893=ORIENTED_EDGE ( 'NONE', *, *, #34022, .F. ) ;
#37969=CARTESIAN_POINT ( 'NONE',  ( 5.000000000000000000, 0.000000000000000000, 0.000000000000000000 ) ) ;
#37999=CARTESIAN_POINT ( 'NONE',  ( 5.000000000000000000, -3.441691376337999159E-14, 1.598721155459999804E-14 ) ) ;
#38020=ORIENTED_EDGE ( 'NONE', *, *, #5201, .T. ) ;
#38021=LINE ( 'NONE', #43629, #61279 ) ;
#38033=DIRECTION ( 'NONE',  ( 0.000000000000000000, -0.2461538461538895495, 0.9692307692307581268 ) ) ;
#38042=AXIS2_PLACEMENT_3D ( 'NONE', #38553, #23509, #65460 ) ;
#38058=ORIENTED_EDGE ( 'NONE', *, *, #24080, .F. ) ;
#38084=ORIENTED_EDGE ( 'NONE', *, *, #64761, .T. ) ;
#38144=DIRECTION ( 'NONE',  ( 1.000000000000000000, 0.000000000000000000, 0.000000000000000000 ) ) ;
#38194=ORIENTED_EDGE ( 'NONE', *, *, #38711, .T. ) ;
#38256=ORIENTED_EDGE ( 'NONE', *, *, #2140, .F. ) ;
#38273=FACE_OUTER_BOUND ( 'NONE', #34471, .T. ) ;
#38286=AXIS2_PLACEMENT_3D ( 'NONE', #33938, #56293, #2122 ) ;
#38319=EDGE_LOOP ( 'NONE', ( #52063, #33631, #9723, #51016 ) ) ;
#38335=( NAMED_UNIT ( * ) PLANE_ANGLE_UNIT ( ) SI_UNIT ( $, .RADIAN. ) );
#38359=VECTOR ( 'NONE', #53511, 1000.000000000000000 ) ;
#38378=VERTEX_POINT ( 'NONE', #59172 ) ;
#38396=DIRECTION ( 'NONE',  ( 1.000000000000000000, 0.000000000000000000, 0.000000000000000000 ) ) ;
#38487=VECTOR ( 'NONE', #51239, 1000.000000000000000 ) ;
#38504=AXIS2_PLACEMENT_3D ( 'NONE', #8866, #67237, #19704 ) ;
#38506=DIRECTION ( 'NONE',  ( 0.000000000000000000, -1.000000000000000000, 0.000000000000000000 ) ) ;
#38541=DIRECTION ( 'NONE',  ( 0.000000000000000000, 0.000000000000000000, 1.000000000000000000 ) ) ;
#38553=CARTESIAN_POINT ( 'NONE',  ( 5.500000000000000000, -1.199999999999999956, 9.776630298829998011 ) ) ;
#38570=EDGE_CURVE ( 'NONE', #42800, #79, #55278, .T. ) ;
#38574=CARTESIAN_POINT ( 'NONE',  ( 5.000000004731000480, 0.05000000473133000417, 3.150000012852999909 ) ) ;
#38608=LINE ( 'NONE', #514, #33108 ) ;
#38618=ORIENTED_EDGE ( 'NONE', *, *, #28897, .T. ) ;
#38632=CARTESIAN_POINT ( 'NONE',  ( 10.90000000000000036, 0.2500000000000000000, -9.776630298829998011 ) ) ;
#38686=VERTEX_POINT ( 'NONE', #52083 ) ;
#38711=EDGE_CURVE ( 'NONE', #16924, #37496, #10129, .T. ) ;
#38779=ORIENTED_EDGE ( 'NONE', *, *, #1827, .F. ) ;
#38848=VECTOR ( 'NONE', #8228, 1000.000000000000000 ) ;
#38914=CARTESIAN_POINT ( 'NONE',  ( 5.000000004241000440, 0.05000000424131000043, -3.149999962200000336 ) ) ;
#38918=EDGE_CURVE ( 'NONE', #59040, #65610, #46340, .T. ) ;
#38982=EDGE_CURVE ( 'NONE', #47459, #53505, #21709, .T. ) ;
#38996=AXIS2_PLACEMENT_3D ( 'NONE', #42617, #5885, #38396 ) ;
#39085=ADVANCED_FACE ( 'NONE', ( #43150 ), #11670, .F. ) ;
#39152=LINE ( 'NONE', #60475, #17093 ) ;
#39332=EDGE_CURVE ( 'NONE', #24493, #34006, #44034, .T. ) ;
#39363=CARTESIAN_POINT ( 'NONE',  ( 5.500000000000000000, -0.2500000000000000000, -3.149999999999999911 ) ) ;
#39405=CARTESIAN_POINT ( 'NONE',  ( 5.500000000000000000, -1.315736040608999957, -10.71955403322999878 ) ) ;
#39448=EDGE_LOOP ( 'NONE', ( #35259, #13623, #5148, #28734, #15255, #56996, #12985, #13715 ) ) ;
#39600=FACE_OUTER_BOUND ( 'NONE', #43512, .T. ) ;
#39655=EDGE_LOOP ( 'NONE', ( #15327, #46358, #5362, #54431 ) ) ;
#39752=CARTESIAN_POINT ( 'NONE',  ( 7.000000000000000000, 0.8000000000000000444, -3.149999999999999911 ) ) ;
#39761=ORIENTED_EDGE ( 'NONE', *, *, #48233, .T. ) ;
#39835=CARTESIAN_POINT ( 'NONE',  ( 5.099999999649000415, -1.199999999999999956, -9.776630298829998011 ) ) ;
#39843=ORIENTED_EDGE ( 'NONE', *, *, #34022, .T. ) ;
#39863=CIRCLE ( 'NONE', #10795, 2.499999999999999556 ) ;
#39925=CIRCLE ( 'NONE', #22027, 0.5500000000000000444 ) ;
#39946=VECTOR ( 'NONE', #32916, 1000.000000000000000 ) ;
#39957=DIRECTION ( 'NONE',  ( 0.000000000000000000, -0.1218274111675001353, 0.9925512993736016476 ) ) ;
#40036=ORIENTED_EDGE ( 'NONE', *, *, #35828, .F. ) ;
#40254=CARTESIAN_POINT ( 'NONE',  ( 7.000000000000000000, -9.735955015381000166, 5.735955015381000166 ) ) ;
#40345=CARTESIAN_POINT ( 'NONE',  ( 0.000000000000000000, 0.000000000000000000, 0.000000000000000000 ) ) ;
#40410=ORIENTED_EDGE ( 'NONE', *, *, #5232, .F. ) ;
#40469=EDGE_CURVE ( 'NONE', #46383, #43332, #67277, .T. ) ;
#40489=ORIENTED_EDGE ( 'NONE', *, *, #27664, .F. ) ;
#40567=CARTESIAN_POINT ( 'NONE',  ( 5.199999999962999553, -1.376649744612000070, -11.21582968308000083 ) ) ;
#40592=EDGE_CURVE ( 'NONE', #13624, #59040, #32237, .T. ) ;
#40601=CARTESIAN_POINT ( 'NONE',  ( 10.90000000000000036, 0.2500000000000000000, 4.902439024389999567 ) ) ;
#40607=VECTOR ( 'NONE', #38541, 1000.000000000000000 ) ;
#40650=CONICAL_SURFACE ( 'NONE', #12769, 2.599999999741000156, 0.7853981633972997312 ) ;
#40658=DIRECTION ( 'NONE',  ( 0.9999999999999998890, 3.212307467389999644E-09, 9.519590337635998530E-09 ) ) ;
#40683=AXIS2_PLACEMENT_3D ( 'NONE', #19740, #51213, #62714 ) ;
#40703=ADVANCED_FACE ( 'NONE', ( #33414 ), #55077, .T. ) ;
#40779=CONICAL_SURFACE ( 'NONE', #10626, 1.699999998954999869, 0.7853981633972997312 ) ;
#40832=ORIENTED_EDGE ( 'NONE', *, *, #34750, .F. ) ;
#40854=DIRECTION ( 'NONE',  ( 0.000000000000000000, 0.000000000000000000, -1.000000000000000000 ) ) ;
#40869=DIRECTION ( 'NONE',  ( 1.000000000000000000, 0.000000000000000000, 0.000000000000000000 ) ) ;
#40923=EDGE_CURVE ( 'NONE', #63702, #23202, #35815, .T. ) ;
#40945=AXIS2_PLACEMENT_3D ( 'NONE', #9953, #50891, #68670 ) ;
#41056=DIRECTION ( 'NONE',  ( 1.000000000000000000, 0.000000000000000000, 0.000000000000000000 ) ) ;
#41073=AXIS2_PLACEMENT_3D ( 'NONE', #39835, #23406, #40854 ) ;
#41088=ORIENTED_EDGE ( 'NONE', *, *, #1827, .T. ) ;
#41105=VERTEX_POINT ( 'NONE', #43393 ) ;
#41149=CARTESIAN_POINT ( 'NONE',  ( 5.000000000000000000, -1.199999999999999956, -11.02663029882999801 ) ) ;
#41207=DIRECTION ( 'NONE',  ( -1.000000000000000000, 0.000000000000000000, 0.000000000000000000 ) ) ;
#41217=ADVANCED_FACE ( 'NONE', ( #61533 ), #12607, .T. ) ;
#41323=CARTESIAN_POINT ( 'NONE',  ( 5.099999999649000415, -1.199999999999999956, -11.12663029847899843 ) ) ;
#41443=LINE ( 'NONE', #57169, #47346 ) ;
#41466=CARTESIAN_POINT ( 'NONE',  ( 10.90000000000000036, -0.2500000000000000000, -4.902439024389999567 ) ) ;
#41502=CIRCLE ( 'NONE', #13677, 2.199999999999999734 ) ;
#41563=ORIENTED_EDGE ( 'NONE', *, *, #59258, .T. ) ;
#41582=DIRECTION ( 'NONE',  ( -1.000000000000000000, 0.000000000000000000, 0.000000000000000000 ) ) ;
#41598=ORIENTED_EDGE ( 'NONE', *, *, #18707, .T. ) ;
#41619=DIRECTION ( 'NONE',  ( 0.000000000000000000, 0.000000000000000000, -1.000000000000000000 ) ) ;
#41660=ADVANCED_FACE ( 'NONE', ( #54050 ), #69097, .F. ) ;
#41698=AXIS2_PLACEMENT_3D ( 'NONE', #16342, #32095, #58998 ) ;
#41712=EDGE_CURVE ( 'NONE', #54437, #59964, #17067, .T. ) ;
#41730=AXIS2_PLACEMENT_3D ( 'NONE', #11802, #10768, #64588 ) ;
#41750=ORIENTED_EDGE ( 'NONE', *, *, #27138, .T. ) ;
#41769=DIRECTION ( 'NONE',  ( 1.000000000000000000, 0.000000000000000000, 0.000000000000000000 ) ) ;
#41917=CARTESIAN_POINT ( 'NONE',  ( 5.200000000000000178, -1.199999999999999956, 9.776630298829998011 ) ) ;
#41947=DIRECTION ( 'NONE',  ( 0.000000000000000000, -0.2461538461537953471, 0.9692307692307821076 ) ) ;
#41981=EDGE_LOOP ( 'NONE', ( #8937, #68346, #66945, #43591 ) ) ;
#42147=ORIENTED_EDGE ( 'NONE', *, *, #10415, .F. ) ;
#42172=CARTESIAN_POINT ( 'NONE',  ( 5.000000004241000440, 0.05000000424131000043, -3.149999962200000336 ) ) ;
#42245=AXIS2_PLACEMENT_3D ( 'NONE', #61955, #18281, #29819 ) ;
#42392=CARTESIAN_POINT ( 'NONE',  ( 5.000000000000000000, -11.29999999999999893, 0.000000000000000000 ) ) ;
#42528=CARTESIAN_POINT ( 'NONE',  ( 10.90000000000000036, -0.2500000000000000000, 9.776630298829998011 ) ) ;
#42533=VECTOR ( 'NONE', #20333, 1000.000000000000000 ) ;
#42545=DIRECTION ( 'NONE',  ( 0.000000000000000000, -1.000000000000000000, 0.000000000000000000 ) ) ;
#42579=EDGE_CURVE ( 'NONE', #16924, #65047, #39863, .T. ) ;
#42608=DIRECTION ( 'NONE',  ( -1.000000000000000000, 0.000000000000000000, 0.000000000000000000 ) ) ;
#42617=CARTESIAN_POINT ( 'NONE',  ( 5.000000000000000000, 0.2500000000000000000, -9.776630298829998011 ) ) ;
#42649=CIRCLE ( 'NONE', #228, 0.9500000000000007327 ) ;
#42699=DIRECTION ( 'NONE',  ( 0.7071067811865459074, -0.08614499000932547557, 0.7018397542860447258 ) ) ;
#42793=AXIS2_PLACEMENT_3D ( 'NONE', #43531, #32016, #48423 ) ;
#42800=VERTEX_POINT ( 'NONE', #15546 ) ;
#42855=ORIENTED_EDGE ( 'NONE', *, *, #38570, .T. ) ;
#42908=AXIS2_PLACEMENT_3D ( 'NONE', #67556, #14439, #18987 ) ;
#43097=AXIS2_PLACEMENT_3D ( 'NONE', #19878, #41207, #67413 ) ;
#43150=FACE_OUTER_BOUND ( 'NONE', #13541, .T. ) ;
#43173=AXIS2_PLACEMENT_3D ( 'NONE', #37999, #33114, #64902 ) ;
#43275=VECTOR ( 'NONE', #3579, 1000.000000000000114 ) ;
#43310=DIRECTION ( 'NONE',  ( 0.000000000000000000, -1.000000000000000000, 0.000000000000000000 ) ) ;
#43332=VERTEX_POINT ( 'NONE', #22148 ) ;
#43393=CARTESIAN_POINT ( 'NONE',  ( 5.500000000000000000, -0.2500000000000000000, 9.776630298829998011 ) ) ;
#43413=CIRCLE ( 'NONE', #33383, 0.7499999999999998890 ) ;
#43418=CARTESIAN_POINT ( 'NONE',  ( 10.90000000000000036, 0.2500000000000000000, 4.902439024389999567 ) ) ;
#43448=ORIENTED_EDGE ( 'NONE', *, *, #11730, .T. ) ;
#43454=LINE ( 'NONE', #68022, #40607 ) ;
#43512=EDGE_LOOP ( 'NONE', ( #37390, #2821, #27609, #30087, #58588 ) ) ;
#43526=ORIENTED_EDGE ( 'NONE', *, *, #11139, .T. ) ;
#43531=CARTESIAN_POINT ( 'NONE',  ( 7.000000000000000000, 0.000000000000000000, 0.000000000000000000 ) ) ;
#43591=ORIENTED_EDGE ( 'NONE', *, *, #43652, .T. ) ;
#43610=APPLICATION_CONTEXT ( 'automotive_design' ) ;
#43621=CARTESIAN_POINT ( 'NONE',  ( 7.307500000000000107, -0.2500000000000000000, 3.149999999999999911 ) ) ;
#43629=CARTESIAN_POINT ( 'NONE',  ( 5.200000002192999737, 0.6646153561348999705, 2.616923086418999844 ) ) ;
#43635=CYLINDRICAL_SURFACE ( 'NONE', #57901, 1.600000000000000089 ) ;
#43652=EDGE_CURVE ( 'NONE', #23202, #18749, #9745, .T. ) ;
#43692=ORIENTED_EDGE ( 'NONE', *, *, #16134, .T. ) ;
#43758=EDGE_CURVE ( 'NONE', #35905, #46383, #55871, .T. ) ;
#43864=VERTEX_POINT ( 'NONE', #69102 ) ;
#43884=VERTEX_POINT ( 'NONE', #50202 ) ;
#43915=ORIENTED_EDGE ( 'NONE', *, *, #29605, .T. ) ;
#43930=FACE_OUTER_BOUND ( 'NONE', #16018, .T. ) ;
#43939=ORIENTED_EDGE ( 'NONE', *, *, #51000, .F. ) ;
#43989=CIRCLE ( 'NONE', #67422, 1.800000000000000044 ) ;
#44001=ORIENTED_EDGE ( 'NONE', *, *, #18479, .F. ) ;
#44002=STYLED_ITEM ( 'NONE', ( #13169 ), #31875 ) ;
#44034=LINE ( 'NONE', #42392, #51557 ) ;
#44056=ADVANCED_FACE ( 'NONE', ( #44627 ), #18046, .T. ) ;
#44097=( GEOMETRIC_REPRESENTATION_CONTEXT ( 3 ) GLOBAL_UNCERTAINTY_ASSIGNED_CONTEXT ( ( #19923 ) ) GLOBAL_UNIT_ASSIGNED_CONTEXT ( ( #46116, #19546, #30723 ) ) REPRESENTATION_CONTEXT ( 'NONE', 'WORKASPACE' ) );
#44168=DIRECTION ( 'NONE',  ( -6.753599194678000463E-10, -6.753597969543999501E-10, -1.000000000000000000 ) ) ;
#44491=CARTESIAN_POINT ( 'NONE',  ( 5.000000000000000000, -1.800000000000000044, 0.000000000000000000 ) ) ;
#44554=CARTESIAN_POINT ( 'NONE',  ( 10.90000000000000036, -1.376649746192999846, 11.21582968292000082 ) ) ;
#44591=CARTESIAN_POINT ( 'NONE',  ( 5.100000000000000533, 0.1499999999999999944, -6.463315149415000072 ) ) ;
#44627=FACE_OUTER_BOUND ( 'NONE', #20829, .T. ) ;
#44654=CARTESIAN_POINT ( 'NONE',  ( 5.500000000000000000, -1.315736040608999957, 10.71955403322999878 ) ) ;
#44713=VERTEX_POINT ( 'NONE', #43418 ) ;
#44961=AXIS2_PLACEMENT_3D ( 'NONE', #46254, #67218, #55366 ) ;
#44984=ORIENTED_EDGE ( 'NONE', *, *, #41712, .T. ) ;
#45131=LINE ( 'NONE', #60513, #13205 ) ;
#45196=DIRECTION ( 'NONE',  ( 1.000000000000000000, 0.000000000000000000, 0.000000000000000000 ) ) ;
#45257=CARTESIAN_POINT ( 'NONE',  ( 7.000000000000000000, 0.5415384615382999867, -2.132307692307999769 ) ) ;
#45258=ORIENTED_EDGE ( 'NONE', *, *, #25484, .F. ) ;
#45476=ORIENTED_EDGE ( 'NONE', *, *, #38711, .F. ) ;
#45535=DIRECTION ( 'NONE',  ( 0.000000000000000000, 1.000000000000000000, 0.000000000000000000 ) ) ;
#45595=FACE_OUTER_BOUND ( 'NONE', #31662, .T. ) ;
#45655=CARTESIAN_POINT ( 'NONE',  ( 5.200000002332999749, 0.2500000023327000331, -3.149999979209999967 ) ) ;
#45756=AXIS2_PLACEMENT_3D ( 'NONE', #60186, #47970, #38506 ) ;
#45783=ADVANCED_FACE ( 'NONE', ( #56221 ), #24406, .T. ) ;
#45843=ADVANCED_FACE ( 'NONE', ( #51319 ), #65639, .F. ) ;
#46027=SHAPE_REPRESENTATION ( 'Insulator', ( #9676 ), #21760 ) ;
#46081=AXIS2_PLACEMENT_3D ( 'NONE', #27147, #31703, #26455 ) ;
#46084=ORIENTED_EDGE ( 'NONE', *, *, #17637, .T. ) ;
#46116=( LENGTH_UNIT ( ) NAMED_UNIT ( * ) SI_UNIT ( .MILLI., .METRE. ) );
#46142=CARTESIAN_POINT ( 'NONE',  ( 7.000000000000000000, 0.2708497377871000311, 3.000000000000000000 ) ) ;
#46182=ORIENTED_EDGE ( 'NONE', *, *, #27664, .T. ) ;
#46188=DIRECTION ( 'NONE',  ( 0.000000000000000000, -0.7626730937533933163, -0.6467841618844942797 ) ) ;
#46200=MECHANICAL_DESIGN_GEOMETRIC_PRESENTATION_REPRESENTATION('',(#44002),#48435);
#46223=CARTESIAN_POINT ( 'NONE',  ( 10.90000000000000036, -8.618205959414002137, -7.308661029293999967 ) ) ;
#46254=CARTESIAN_POINT ( 'NONE',  ( 5.200000000000000178, 0.000000000000000000, 0.000000000000000000 ) ) ;
#46330=MECHANICAL_DESIGN_GEOMETRIC_PRESENTATION_REPRESENTATION('',(#6139),#44097);
#46340=LINE ( 'NONE', #56832, #38487 ) ;
#46358=ORIENTED_EDGE ( 'NONE', *, *, #58923, .F. ) ;
#46374=VERTEX_POINT ( 'NONE', #44554 ) ;
#46383=VERTEX_POINT ( 'NONE', #45257 ) ;
#46486=CARTESIAN_POINT ( 'NONE',  ( 7.066756274120936432, 0.2616187012132839551, 3.032564036156813803 ) ) ;
#46565=LINE ( 'NONE', #61269, #804 ) ;
#46680=DIRECTION ( 'NONE',  ( 0.000000000000000000, 1.000000000000000000, 0.000000000000000000 ) ) ;
#46719=FACE_OUTER_BOUND ( 'NONE', #55408, .T. ) ;
#46736=CARTESIAN_POINT ( 'NONE',  ( 5.000000001445999764, -1.799999998554000058, 4.283816198543999816E-09 ) ) ;
#46888=CARTESIAN_POINT ( 'NONE',  ( 7.000000000000000000, -9.370210309074998634, -5.370210309075000410 ) ) ;
#46907=ADVANCED_BREP_SHAPE_REPRESENTATION ( '', ( #31875, #9676 ), #21760 ) ;
#46944=FACE_OUTER_BOUND ( 'NONE', #9464, .T. ) ;
#47019=CARTESIAN_POINT ( 'NONE',  ( 5.200000000000000178, 0.000000000000000000, -1.600000000000000089 ) ) ;
#47032=ORIENTED_EDGE ( 'NONE', *, *, #64153, .T. ) ;
#47103=DIRECTION ( 'NONE',  ( 0.000000000000000000, 1.000000000000000000, 0.000000000000000000 ) ) ;
#47169=ORIENTED_EDGE ( 'NONE', *, *, #2599, .T. ) ;
#47230=ORIENTED_EDGE ( 'NONE', *, *, #42579, .F. ) ;
#47339=PLANE ( 'NONE',  #67829 ) ;
#47346=VECTOR ( 'NONE', #19428, 1000.000000000000000 ) ;
#47387=DIRECTION ( 'NONE',  ( 0.000000000000000000, 0.2461538461537955691, -0.9692307692307821076 ) ) ;
#47413=LINE ( 'NONE', #42172, #14764 ) ;
#47456=EDGE_LOOP ( 'NONE', ( #26951, #21370, #23572, #32933 ) ) ;
#47459=VERTEX_POINT ( 'NONE', #7751 ) ;
#47682=LINE ( 'NONE', #57463, #51178 ) ;
#47824=DIRECTION ( 'NONE',  ( 0.000000000000000000, -1.000000000000000000, 0.000000000000000000 ) ) ;
#47871=CARTESIAN_POINT ( 'NONE',  ( 5.000000000000000000, 0.000000000000000000, 0.000000000000000000 ) ) ;
#47876=DIRECTION ( 'NONE',  ( 0.000000000000000000, 1.000000000000000000, 0.000000000000000000 ) ) ;
#47970=DIRECTION ( 'NONE',  ( 1.000000000000000000, 0.000000000000000000, 0.000000000000000000 ) ) ;
#48005=ORIENTED_EDGE ( 'NONE', *, *, #10269, .F. ) ;
#48129=EDGE_CURVE ( 'NONE', #52415, #30037, #64006, .T. ) ;
#48131=DIRECTION ( 'NONE',  ( -1.000000000000000000, 0.000000000000000000, 0.000000000000000000 ) ) ;
#48142=ORIENTED_EDGE ( 'NONE', *, *, #11730, .F. ) ;
#48153=CYLINDRICAL_SURFACE ( 'NONE', #11879, 1.449999999999999734 ) ;
#48197=ORIENTED_EDGE ( 'NONE', *, *, #30925, .T. ) ;
#48226=CARTESIAN_POINT ( 'NONE',  ( 5.100000001045000175, 0.000000000000000000, 0.000000000000000000 ) ) ;
#48233=EDGE_CURVE ( 'NONE', #68795, #7995, #49312, .T. ) ;
#48242=CIRCLE ( 'NONE', #8083, 1.800000000000000044 ) ;
#48298=CARTESIAN_POINT ( 'NONE',  ( 7.000000000000000000, 0.000000000000000000, 0.000000000000000000 ) ) ;
#48417=ORIENTED_EDGE ( 'NONE', *, *, #64332, .T. ) ;
#48423=DIRECTION ( 'NONE',  ( 0.000000000000000000, 0.2461538461537955691, -0.9692307692307821076 ) ) ;
#48435=( GEOMETRIC_REPRESENTATION_CONTEXT ( 3 ) GLOBAL_UNCERTAINTY_ASSIGNED_CONTEXT ( ( #55353 ) ) GLOBAL_UNIT_ASSIGNED_CONTEXT ( ( #65933, #38335, #7558 ) ) REPRESENTATION_CONTEXT ( 'NONE', 'WORKASPACE' ) );
#48519=VECTOR ( 'NONE', #2476, 1000.000000000000000 ) ;
#48566=ORIENTED_EDGE ( 'NONE', *, *, #37701, .F. ) ;
#48712=CARTESIAN_POINT ( 'NONE',  ( 5.200000000000000178, -1.199999999999999956, -11.22663029882996710 ) ) ;
#48769=VERTEX_POINT ( 'NONE', #38574 ) ;
#48830=AXIS2_PLACEMENT_3D ( 'NONE', #59727, #53459, #47876 ) ;
#48835=ORIENTED_EDGE ( 'NONE', *, *, #2319, .F. ) ;
#48848=ORIENTED_EDGE ( 'NONE', *, *, #52310, .T. ) ;
#49007=ORIENTED_EDGE ( 'NONE', *, *, #43758, .T. ) ;
#49128=VERTEX_POINT ( 'NONE', #36779 ) ;
#49176=CIRCLE ( 'NONE', #6747, 0.5500000000000001554 ) ;
#49312=LINE ( 'NONE', #65033, #24083 ) ;
#49389=CARTESIAN_POINT ( 'NONE',  ( 5.000000000000000000, -1.352284263959000032, 11.01731942304999912 ) ) ;
#49398=CARTESIAN_POINT ( 'NONE',  ( 10.90000000000000036, -8.263403946409999534, -6.953859016290999229 ) ) ;
#49476=EDGE_CURVE ( 'NONE', #3659, #64075, #36065, .T. ) ;
#49629=CYLINDRICAL_SURFACE ( 'NONE', #67847, 1.600000000000000089 ) ;
#49762=VECTOR ( 'NONE', #63102, 1000.000000000000114 ) ;
#49906=DIRECTION ( 'NONE',  ( 1.000000000000000000, 0.000000000000000000, 0.000000000000000000 ) ) ;
#49995=VECTOR ( 'NONE', #8957, 1000.000000000000000 ) ;
#50012=AXIS2_PLACEMENT_3D ( 'NONE', #22093, #37835, #65778 ) ;
#50046=ADVANCED_FACE ( 'NONE', ( #14984, #9050 ), #8717, .T. ) ;
#50086=CARTESIAN_POINT ( 'NONE',  ( 5.000000000000000000, 0.000000000000000000, -1.799999999999970512 ) ) ;
#50202=CARTESIAN_POINT ( 'NONE',  ( 5.500000000000000000, -0.2500000000000000000, -3.149999999999999911 ) ) ;
#50207=CYLINDRICAL_SURFACE ( 'NONE', #28678, 1.050000000000000044 ) ;
#50216=EDGE_CURVE ( 'NONE', #56969, #64650, #37004, .T. ) ;
#50290=DIRECTION ( 'NONE',  ( 0.000000000000000000, 0.000000000000000000, -1.000000000000000000 ) ) ;
#50400=CARTESIAN_POINT ( 'NONE',  ( 10.90000000000000036, -8.618205959414002137, 7.308661029293999967 ) ) ;
#50539=AXIS2_PLACEMENT_3D ( 'NONE', #39752, #28932, #27885 ) ;
#50550=ORIENTED_EDGE ( 'NONE', *, *, #50216, .F. ) ;
#50579=CARTESIAN_POINT ( 'NONE',  ( 5.200000000000000178, 0.000000000000000000, 0.000000000000000000 ) ) ;
#50666=DIRECTION ( 'NONE',  ( 0.000000000000000000, -0.8615889394142682844, 0.5076066385292812289 ) ) ;
#50670=DIRECTION ( 'NONE',  ( 1.000000000000000000, 0.000000000000000000, 0.000000000000000000 ) ) ;
#50679=AXIS2_PLACEMENT_3D ( 'NONE', #27229, #10796, #43310 ) ;
#50744=CARTESIAN_POINT ( 'NONE',  ( 10.90000000000000036, -1.376649746192999846, -11.21582968292000082 ) ) ;
#50837=ORIENTED_EDGE ( 'NONE', *, *, #64332, .F. ) ;
#50891=DIRECTION ( 'NONE',  ( 1.000000000000000000, 0.000000000000000000, 0.000000000000000000 ) ) ;
#50893=CARTESIAN_POINT ( 'NONE',  ( 5.500000000000000000, -1.199999999999999956, 9.776630298829998011 ) ) ;
#51000=EDGE_CURVE ( 'NONE', #59964, #14358, #35893, .T. ) ;
#51016=ORIENTED_EDGE ( 'NONE', *, *, #52410, .F. ) ;
#51119=CARTESIAN_POINT ( 'NONE',  ( 7.307500000000000107, 0.2500000000000000000, 3.149999999999999911 ) ) ;
#51160=LINE ( 'NONE', #67221, #9635 ) ;
#51161=CARTESIAN_POINT ( 'NONE',  ( 5.000000000000000000, 0.000000000000000000, 0.000000000000000000 ) ) ;
#51178=VECTOR ( 'NONE', #63042, 1000.000000000000000 ) ;
#51213=DIRECTION ( 'NONE',  ( -1.000000000000000000, 0.000000000000000000, 0.000000000000000000 ) ) ;
#51239=DIRECTION ( 'NONE',  ( 4.129963865151999738E-10, 4.129962357295999768E-10, -1.000000000000000000 ) ) ;
#51240=ADVANCED_FACE ( 'NONE', ( #10610 ), #47339, .T. ) ;
#51245=ORIENTED_EDGE ( 'NONE', *, *, #16578, .F. ) ;
#51319=FACE_OUTER_BOUND ( 'NONE', #1240, .T. ) ;
#51343=CARTESIAN_POINT ( 'NONE',  ( 7.000000000000000000, 0.6646153846154000400, 2.616923076922999858 ) ) ;
#51464=DIRECTION ( 'NONE',  ( 1.000000000000000000, 4.438568037851000240E-10, 1.557552607591000152E-09 ) ) ;
#51472=CIRCLE ( 'NONE', #4548, 1.600000000000000089 ) ;
#51522=EDGE_CURVE ( 'NONE', #62590, #11166, #21537, .T. ) ;
#51538=ORIENTED_EDGE ( 'NONE', *, *, #48129, .F. ) ;
#51557=VECTOR ( 'NONE', #65337, 1000.000000000000000 ) ;
#51603=ADVANCED_FACE ( 'NONE', ( #6142 ), #4763, .T. ) ;
#51655=DIRECTION ( 'NONE',  ( 0.4384236320213992233, -0.6355252626312997144, -0.6355252626312997144 ) ) ;
#51676=CIRCLE ( 'NONE', #34982, 11.29999999999999538 ) ;
#51679=EDGE_LOOP ( 'NONE', ( #62139, #38618, #43939, #32295 ) ) ;
#51695=SURFACE_STYLE_USAGE ( .BOTH. , #8712 ) ;
#51728=AXIS2_PLACEMENT_3D ( 'NONE', #58223, #5430, #16605 ) ;
#51776=EDGE_CURVE ( 'NONE', #30122, #43332, #57478, .T. ) ;
#51883=CARTESIAN_POINT ( 'NONE',  ( 5.200000002332999749, 0.2500000023327000331, -3.149999979209999967 ) ) ;
#51884=VECTOR ( 'NONE', #47824, 1000.000000000000000 ) ;
#51932=ORIENTED_EDGE ( 'NONE', *, *, #2357, .F. ) ;
#51961=CARTESIAN_POINT ( 'NONE',  ( 5.200000000000000178, -11.29999999999999893, 0.000000000000000000 ) ) ;
#52002=AXIS2_PLACEMENT_3D ( 'NONE', #22139, #821, #59198 ) ;
#52012=VERTEX_POINT ( 'NONE', #25247 ) ;
#52063=ORIENTED_EDGE ( 'NONE', *, *, #2319, .T. ) ;
#52064=AXIS2_PLACEMENT_3D ( 'NONE', #3796, #40869, #4480 ) ;
#52083=CARTESIAN_POINT ( 'NONE',  ( 10.90000000000000036, 0.2500000000000000000, 9.776630298829998011 ) ) ;
#52224=AXIS2_PLACEMENT_3D ( 'NONE', #4043, #30298, #36218 ) ;
#52280=CARTESIAN_POINT ( 'NONE',  ( 4.999999999955999641, -1.352284261683000199, -11.01731942327999825 ) ) ;
#52294=DIRECTION ( 'NONE',  ( 0.000000000000000000, 0.000000000000000000, -1.000000000000000000 ) ) ;
#52295=CARTESIAN_POINT ( 'NONE',  ( 7.000000000000000000, 0.2708497377871000311, -3.000000000000000000 ) ) ;
#52298=ORIENTED_EDGE ( 'NONE', *, *, #25835, .T. ) ;
#52310=EDGE_CURVE ( 'NONE', #13624, #48769, #47682, .T. ) ;
#52359=CIRCLE ( 'NONE', #16624, 1.250000000000000000 ) ;
#52381=( NAMED_UNIT ( * ) PLANE_ANGLE_UNIT ( ) SI_UNIT ( $, .RADIAN. ) );
#52409=CARTESIAN_POINT ( 'NONE',  ( 7.169256274120936467, 0.2500000000000000000, 3.082564036157276366 ) ) ;
#52410=EDGE_CURVE ( 'NONE', #52012, #8057, #28782, .T. ) ;
#52415=VERTEX_POINT ( 'NONE', #49389 ) ;
#52619=VECTOR ( 'NONE', #65882, 1000.000000000000000 ) ;
#52642=ADVANCED_FACE ( 'NONE', ( #39600 ), #66162, .T. ) ;
#52779=DIRECTION ( 'NONE',  ( 0.7071067811865180408, 0.1740571194759044926, 0.6853496327859179837 ) ) ;
#52950=CARTESIAN_POINT ( 'NONE',  ( 5.199999999795999805, 0.2499999997964000020, -9.776630293835998131 ) ) ;
#52991=CARTESIAN_POINT ( 'NONE',  ( 7.000000000000000000, 3.640000000000000124, -3.000000000000000000 ) ) ;
#52994=ORIENTED_EDGE ( 'NONE', *, *, #67430, .F. ) ;
#53000=DIRECTION ( 'NONE',  ( -1.000000000000000000, 0.000000000000000000, 0.000000000000000000 ) ) ;
#53020=ORIENTED_EDGE ( 'NONE', *, *, #27794, .T. ) ;
#53078=LINE ( 'NONE', #36659, #31623 ) ;
#53177=ADVANCED_FACE ( 'NONE', ( #64430 ), #63144, .F. ) ;
#53245=ORIENTED_EDGE ( 'NONE', *, *, #40592, .T. ) ;
#53425=CARTESIAN_POINT ( 'NONE',  ( 7.000000000000000000, 0.2708497377871000311, -3.000000000000000000 ) ) ;
#53459=DIRECTION ( 'NONE',  ( -1.000000000000000000, 0.000000000000000000, 0.000000000000000000 ) ) ;
#53505=VERTEX_POINT ( 'NONE', #12272 ) ;
#53506=LINE ( 'NONE', #46888, #6803 ) ;
#53511=DIRECTION ( 'NONE',  ( 0.000000000000000000, -1.000000000000000000, 0.000000000000000000 ) ) ;
#53607=CARTESIAN_POINT ( 'NONE',  ( 7.000000000000000000, -9.735955015381000166, 5.735955015381000166 ) ) ;
#53625=AXIS2_PLACEMENT_3D ( 'NONE', #36170, #4682, #24992 ) ;
#53654=DIRECTION ( 'NONE',  ( -0.8987684456439055669, 0.000000000000000000, -0.4384236320214022764 ) ) ;
#53685=DIRECTION ( 'NONE',  ( 0.000000000000000000, -0.1218274111675000937, 0.9925512993736016476 ) ) ;
#53687=DIRECTION ( 'NONE',  ( 0.000000000000000000, -1.000000000000000000, 0.000000000000000000 ) ) ;
#53740=DIRECTION ( 'NONE',  ( 1.000000000000000000, 0.000000000000000000, 0.000000000000000000 ) ) ;
#53831=AXIS2_PLACEMENT_3D ( 'NONE', #60060, #16705, #38033 ) ;
#53910=AXIS2_PLACEMENT_3D ( 'NONE', #66506, #54646, #39957 ) ;
#54038=EDGE_CURVE ( 'NONE', #13996, #18320, #18840, .T. ) ;
#54045=EDGE_LOOP ( 'NONE', ( #53245, #11558, #31561, #17479 ) ) ;
#54050=FACE_OUTER_BOUND ( 'NONE', #34510, .T. ) ;
#54103=ORIENTED_EDGE ( 'NONE', *, *, #5201, .F. ) ;
#54105=DIRECTION ( 'NONE',  ( 0.9999999999999998890, 1.582250227828999695E-08, -5.275446505821999214E-09 ) ) ;
#54431=ORIENTED_EDGE ( 'NONE', *, *, #34097, .F. ) ;
#54437=VERTEX_POINT ( 'NONE', #15599 ) ;
#54597=ORIENTED_EDGE ( 'NONE', *, *, #43652, .F. ) ;
#54646=DIRECTION ( 'NONE',  ( 1.000000000000000000, 0.000000000000000000, 0.000000000000000000 ) ) ;
#54685=DIRECTION ( 'NONE',  ( 1.000000000000000000, 0.000000000000000000, 0.000000000000000000 ) ) ;
#54702=EDGE_LOOP ( 'NONE', ( #41750, #2689, #48848, #43915, #6437, #43526, #6855, #7844, #35208 ) ) ;
#54762=ORIENTED_EDGE ( 'NONE', *, *, #51522, .F. ) ;
#54770=ORIENTED_EDGE ( 'NONE', *, *, #10559, .T. ) ;
#54778=EDGE_CURVE ( 'NONE', #8057, #36962, #52359, .T. ) ;
#54820=AXIS2_PLACEMENT_3D ( 'NONE', #56461, #29216, #8565 ) ;
#54887=ADVANCED_FACE ( 'NONE', ( #32474 ), #21285, .T. ) ;
#54999=ORIENTED_EDGE ( 'NONE', *, *, #27138, .F. ) ;
#55012=AXIS2_PLACEMENT_3D ( 'NONE', #37969, #59987, #5121 ) ;
#55077=PLANE ( 'NONE',  #63879 ) ;
#55145=CARTESIAN_POINT ( 'NONE',  ( 7.307500000000000107, 0.2500000000000000000, -3.149999999999999911 ) ) ;
#55185=CIRCLE ( 'NONE', #42908, 10.80000000000000604 ) ;
#55241=VERTEX_POINT ( 'NONE', #20516 ) ;
#55278=LINE ( 'NONE', #40567, #48519 ) ;
#55353=UNCERTAINTY_MEASURE_WITH_UNIT (LENGTH_MEASURE( 1.000000000000000082E-05 ), #65933, 'distance_accuracy_value', 'NONE');
#55366=DIRECTION ( 'NONE',  ( 0.000000000000000000, 1.000000000000000000, 0.000000000000000000 ) ) ;
#55374=FACE_OUTER_BOUND ( 'NONE', #9201, .T. ) ;
#55408=EDGE_LOOP ( 'NONE', ( #27578, #3888, #2837, #61506, #24857, #18204, #6725, #20223, #16755 ) ) ;
#55461=SURFACE_STYLE_USAGE ( .BOTH. , #6865 ) ;
#55621=CARTESIAN_POINT ( 'NONE',  ( 9.360840674114749405, -8.748618759363491648, 6.377268954453214178 ) ) ;
#55661=EDGE_LOOP ( 'NONE', ( #6538, #64847, #31029, #66711, #60908, #28129 ) ) ;
#55675=ORIENTED_EDGE ( 'NONE', *, *, #3605, .T. ) ;
#55704=ORIENTED_EDGE ( 'NONE', *, *, #28897, .F. ) ;
#55794=ADVANCED_FACE ( 'NONE', ( #6675 ), #28361, .T. ) ;
#55871=LINE ( 'NONE', #2382, #27628 ) ;
#55882=DIRECTION ( 'NONE',  ( -1.000000000000000000, 0.000000000000000000, 0.000000000000000000 ) ) ;
#56097=EDGE_CURVE ( 'NONE', #48769, #65610, #45131, .T. ) ;
#56111=AXIS2_PLACEMENT_3D ( 'NONE', #48298, #38144, #27323 ) ;
#56113=DIRECTION ( 'NONE',  ( 0.000000000000000000, -0.2461538461537953471, 0.9692307692307821076 ) ) ;
#56221=FACE_OUTER_BOUND ( 'NONE', #64049, .T. ) ;
#56256=DIRECTION ( 'NONE',  ( 1.000000000000000000, 0.000000000000000000, 0.000000000000000000 ) ) ;
#56293=DIRECTION ( 'NONE',  ( 0.000000000000000000, -1.000000000000000000, 0.000000000000000000 ) ) ;
#56446=ORIENTED_EDGE ( 'NONE', *, *, #61091, .F. ) ;
#56461=CARTESIAN_POINT ( 'NONE',  ( 5.000000000000000000, 0.8000000000000000444, 3.149999999999999911 ) ) ;
#56605=FILL_AREA_STYLE ('',( #9380 ) ) ;
#56751=ADVANCED_FACE ( 'NONE', ( #43930 ), #50207, .T. ) ;
#56790=CARTESIAN_POINT ( 'NONE',  ( 5.500000000000000000, -0.2500000000000000000, 3.149999999999999911 ) ) ;
#56832=CARTESIAN_POINT ( 'NONE',  ( 5.199999999864999722, 0.2499999998655000055, 9.776630292580000159 ) ) ;
#56969=VERTEX_POINT ( 'NONE', #47019 ) ;
#56996=ORIENTED_EDGE ( 'NONE', *, *, #58923, .T. ) ;
#56998=EDGE_CURVE ( 'NONE', #34006, #4545, #36492, .T. ) ;
#57030=CARTESIAN_POINT ( 'NONE',  ( 5.200000000000000178, 0.2500000000000000000, -3.149999999999999911 ) ) ;
#57060=VECTOR ( 'NONE', #23759, 1000.000000000000000 ) ;
#57110=AXIS2_PLACEMENT_3D ( 'NONE', #36140, #30553, #7858 ) ;
#57113=EDGE_LOOP ( 'NONE', ( #63405, #5133, #592, #19359, #20867, #28340 ) ) ;
#57137=VERTEX_POINT ( 'NONE', #22155 ) ;
#57146=DIRECTION ( 'NONE',  ( 0.7071067811865474617, -0.7071067811865474617, 5.048524301881336257E-09 ) ) ;
#57169=CARTESIAN_POINT ( 'NONE',  ( 10.90000000000000036, -8.618205959414002137, 7.308661029293999967 ) ) ;
#57198=DIRECTION ( 'NONE',  ( 0.000000000000000000, 0.000000000000000000, -1.000000000000000000 ) ) ;
#57218=DIRECTION ( 'NONE',  ( 1.000000000000000000, 0.000000000000000000, 0.000000000000000000 ) ) ;
#57227=EDGE_CURVE ( 'NONE', #14358, #22158, #21810, .T. ) ;
#57257=EDGE_LOOP ( 'NONE', ( #54762, #50837, #47032, #52298, #58205 ) ) ;
#57290=CONICAL_SURFACE ( 'NONE', #9278, 11.19999999998000106, 0.7853981633972997312 ) ;
#57381=DIRECTION ( 'NONE',  ( -0.8987684456439055669, 0.000000000000000000, -0.4384236320214022764 ) ) ;
#57463=CARTESIAN_POINT ( 'NONE',  ( 4.999999999844999543, 0.04999999984535999364, 9.776630291645998838 ) ) ;
#57478=LINE ( 'NONE', #24303, #38848 ) ;
#57535=CIRCLE ( 'NONE', #67561, 0.9500000000000007327 ) ;
#57872=CARTESIAN_POINT ( 'NONE',  ( 5.500000000000000000, 0.000000000000000000, 0.000000000000000000 ) ) ;
#57901=AXIS2_PLACEMENT_3D ( 'NONE', #33143, #49906, #60738 ) ;
#57989=EDGE_LOOP ( 'NONE', ( #65065, #43448, #37543, #64291, #29304, #39843, #55675, #35116 ) ) ;
#58034=DIRECTION ( 'NONE',  ( 0.000000000000000000, 0.000000000000000000, -1.000000000000000000 ) ) ;
#58065=DIRECTION ( 'NONE',  ( 0.000000000000000000, 0.000000000000000000, -1.000000000000000000 ) ) ;
#58198=DIRECTION ( 'NONE',  ( 1.000000000000000000, 0.000000000000000000, 0.000000000000000000 ) ) ;
#58205=ORIENTED_EDGE ( 'NONE', *, *, #24805, .F. ) ;
#58223=CARTESIAN_POINT ( 'NONE',  ( 5.099999999649000415, -1.199999999999999956, -9.776630298829998011 ) ) ;
#58305=EDGE_CURVE ( 'NONE', #38378, #3659, #41443, .T. ) ;
#58315=CIRCLE ( 'NONE', #50539, 1.049999999999999822 ) ;
#58317=CARTESIAN_POINT ( 'NONE',  ( 5.000000000000000000, 0.8000000000000000444, -3.149999999999999911 ) ) ;
#58322=CIRCLE ( 'NONE', #4709, 1.600000000000000089 ) ;
#58373=EDGE_LOOP ( 'NONE', ( #28566, #21790, #64647, #51932 ) ) ;
#58520=LINE ( 'NONE', #14848, #10110 ) ;
#58588=ORIENTED_EDGE ( 'NONE', *, *, #38918, .F. ) ;
#58601=CARTESIAN_POINT ( 'NONE',  ( 5.000000000000000000, 0.000000000000000000, 0.000000000000000000 ) ) ;
#58612=ADVANCED_FACE ( 'NONE', ( #22863 ), #18324, .T. ) ;
#58628=DIRECTION ( 'NONE',  ( 1.000000000000000000, 0.000000000000000000, 0.000000000000000000 ) ) ;
#58645=ADVANCED_FACE ( 'NONE', ( #12036 ), #40650, .T. ) ;
#58675=DIRECTION ( 'NONE',  ( 0.000000000000000000, -1.000000000000000000, 0.000000000000000000 ) ) ;
#58714=FACE_OUTER_BOUND ( 'NONE', #5699, .T. ) ;
#58923=EDGE_CURVE ( 'NONE', #7995, #64186, #33982, .T. ) ;
#58932=CARTESIAN_POINT ( 'NONE',  ( 5.500000000000000000, 0.000000000000000000, 0.000000000000000000 ) ) ;
#58937=CIRCLE ( 'NONE', #62284, 11.29999999999999538 ) ;
#58998=DIRECTION ( 'NONE',  ( 0.000000000000000000, 1.000000000000000000, 0.000000000000000000 ) ) ;
#59013=CARTESIAN_POINT ( 'NONE',  ( 5.000000000000000000, -1.352284263959000032, -11.01731942304999912 ) ) ;
#59040=VERTEX_POINT ( 'NONE', #60963 ) ;
#59095=ADVANCED_FACE ( 'NONE', ( #55374 ), #30526, .T. ) ;
#59098=DIRECTION ( 'NONE',  ( 1.000000000000000000, 0.000000000000000000, 0.000000000000000000 ) ) ;
#59117=CIRCLE ( 'NONE', #7776, 1.600000000000000089 ) ;
#59172=CARTESIAN_POINT ( 'NONE',  ( 10.90000000000000036, -8.618205959414002137, 7.308661029293999967 ) ) ;
#59198=DIRECTION ( 'NONE',  ( -0.8987684456439056779, 0.000000000000000000, 0.4384236320214023319 ) ) ;
#59200=VECTOR ( 'NONE', #41056, 1000.000000000000000 ) ;
#59258=EDGE_CURVE ( 'NONE', #8285, #24513, #24343, .T. ) ;
#59263=CARTESIAN_POINT ( 'NONE',  ( 10.90000000000000036, -1.199999999999999956, 9.776630298829998011 ) ) ;
#59299=CARTESIAN_POINT ( 'NONE',  ( 5.000000000000000000, 0.000000000000000000, 0.000000000000000000 ) ) ;
#59428=EDGE_CURVE ( 'NONE', #38686, #59040, #15222, .T. ) ;
#59490=ORIENTED_EDGE ( 'NONE', *, *, #10523, .T. ) ;
#59575=EDGE_LOOP ( 'NONE', ( #46182, #36620, #64416, #51538, #54999 ) ) ;
#59655=ORIENTED_EDGE ( 'NONE', *, *, #18539, .F. ) ;
#59713=VECTOR ( 'NONE', #66642, 1000.000000000000000 ) ;
#59727=CARTESIAN_POINT ( 'NONE',  ( 5.200000000000000178, -1.199999999999999956, -9.776630298829998011 ) ) ;
#59739=ADVANCED_FACE ( 'NONE', ( #45595 ), #67928, .T. ) ;
#59817=DIRECTION ( 'NONE',  ( 0.000000000000000000, 1.000000000000000000, 0.000000000000000000 ) ) ;
#59890=CIRCLE ( 'NONE', #43173, 11.10000000000000675 ) ;
#59916=LINE ( 'NONE', #23549, #29877 ) ;
#59964=VERTEX_POINT ( 'NONE', #44491 ) ;
#59987=DIRECTION ( 'NONE',  ( 1.000000000000000000, 0.000000000000000000, 0.000000000000000000 ) ) ;
#60060=CARTESIAN_POINT ( 'NONE',  ( 5.500000000000000000, 0.8000000000000000444, -3.149999999999999911 ) ) ;
#60186=CARTESIAN_POINT ( 'NONE',  ( 5.500000000000000000, 0.8000000000000000444, 3.149999999999999911 ) ) ;
#60235=DIRECTION ( 'NONE',  ( 0.000000000000000000, -0.1218274111675000937, -0.9925512993736016476 ) ) ;
#60238=LINE ( 'NONE', #53607, #17958 ) ;
#60244=CARTESIAN_POINT ( 'NONE',  ( 9.581163468719386955, -9.035708932181607977, -6.816351070799541390 ) ) ;
#60278=ORIENTED_EDGE ( 'NONE', *, *, #34750, .T. ) ;
#60305=LINE ( 'NONE', #38632, #52619 ) ;
#60366=DIRECTION ( 'NONE',  ( 0.000000000000000000, -1.000000000000000000, 0.000000000000000000 ) ) ;
#60475=CARTESIAN_POINT ( 'NONE',  ( 5.500000000000000000, -0.2500000000000000000, 9.776630298829998011 ) ) ;
#60484=ORIENTED_EDGE ( 'NONE', *, *, #62668, .F. ) ;
#60513=CARTESIAN_POINT ( 'NONE',  ( 5.000000004731000480, 0.05000000473133000417, 3.150000012852999909 ) ) ;
#60597=ORIENTED_EDGE ( 'NONE', *, *, #15998, .F. ) ;
#60649=PLANE ( 'NONE',  #60898 ) ;
#60667=VECTOR ( 'NONE', #8926, 1000.000000000000114 ) ;
#60676=ORIENTED_EDGE ( 'NONE', *, *, #67430, .T. ) ;
#60738=DIRECTION ( 'NONE',  ( 0.000000000000000000, -1.000000000000000000, 0.000000000000000000 ) ) ;
#60783=ORIENTED_EDGE ( 'NONE', *, *, #10269, .T. ) ;
#60804=ORIENTED_EDGE ( 'NONE', *, *, #58305, .F. ) ;
#60898=AXIS2_PLACEMENT_3D ( 'NONE', #44591, #18695, #8201 ) ;
#60908=ORIENTED_EDGE ( 'NONE', *, *, #6291, .F. ) ;
#60911=ORIENTED_EDGE ( 'NONE', *, *, #38982, .F. ) ;
#60951=DIRECTION ( 'NONE',  ( -1.000000000000000000, 0.000000000000000000, 0.000000000000000000 ) ) ;
#60959=DIRECTION ( 'NONE',  ( 1.000000000000000000, -4.255854927730000031E-14, 1.480297366167000132E-14 ) ) ;
#60963=CARTESIAN_POINT ( 'NONE',  ( 5.200000000000000178, 0.2500000000000000000, 9.776630298829998011 ) ) ;
#61007=B_SPLINE_CURVE_WITH_KNOTS ( 'NONE', 3,
 ( #2505, #66472, #18596, #13356 ),
 .UNSPECIFIED., .F., .F.,
 ( 4, 4 ),
 ( 0.000000000000000000, 1.000000000000000000 ),
 .UNSPECIFIED. ) ;
#61015=DIRECTION ( 'NONE',  ( -1.000000000000000000, 0.000000000000000000, 0.000000000000000000 ) ) ;
#61069=DIRECTION ( 'NONE',  ( 0.000000000000000000, -0.1218274111675001353, -0.9925512993736016476 ) ) ;
#61091=EDGE_CURVE ( 'NONE', #5290, #63702, #2825, .T. ) ;
#61183=PRODUCT ( 'Insulator', 'Insulator', '', ( #19765 ) ) ;
#61236=CARTESIAN_POINT ( 'NONE',  ( 10.90000000000000036, 0.000000000000000000, 0.000000000000000000 ) ) ;
#61269=CARTESIAN_POINT ( 'NONE',  ( 10.90000000000000036, -0.2500000000000000000, 4.902439024389999567 ) ) ;
#61279=VECTOR ( 'NONE', #54105, 1000.000000000000114 ) ;
#61374=DIRECTION ( 'NONE',  ( 1.000000000000000000, 0.000000000000000000, 0.000000000000000000 ) ) ;
#61383=DIRECTION ( 'NONE',  ( 1.000000000000000000, 0.000000000000000000, 0.000000000000000000 ) ) ;
#61477=EDGE_LOOP ( 'NONE', ( #38194, #35741, #45258, #47230 ) ) ;
#61500=FACE_OUTER_BOUND ( 'NONE', #14899, .T. ) ;
#61506=ORIENTED_EDGE ( 'NONE', *, *, #38982, .T. ) ;
#61533=FACE_OUTER_BOUND ( 'NONE', #57257, .T. ) ;
#61622=EDGE_CURVE ( 'NONE', #8057, #23202, #9416, .T. ) ;
#61634=CARTESIAN_POINT ( 'NONE',  ( 5.000000000000000000, -1.199999999999999956, 9.776630298829998011 ) ) ;
#61805=ORIENTED_EDGE ( 'NONE', *, *, #27794, .F. ) ;
#61818=ORIENTED_EDGE ( 'NONE', *, *, #28353, .F. ) ;
#61847=CARTESIAN_POINT ( 'NONE',  ( 5.200000002601999682, 0.2500000026021999555, 3.150000007068999963 ) ) ;
#61927=DIRECTION ( 'NONE',  ( 0.000000000000000000, -1.000000000000000000, 0.000000000000000000 ) ) ;
#61955=CARTESIAN_POINT ( 'NONE',  ( 5.000000000000000000, 0.2500000000000000000, 3.149999999999999911 ) ) ;
#61991=CYLINDRICAL_SURFACE ( 'NONE', #10881, 11.29999999999999893 ) ;
#62014=ORIENTED_EDGE ( 'NONE', *, *, #56097, .T. ) ;
#62139=ORIENTED_EDGE ( 'NONE', *, *, #18479, .T. ) ;
#62148=CARTESIAN_POINT ( 'NONE',  ( 5.100000001045000175, 0.000000000000000000, 0.000000000000000000 ) ) ;
#62284=AXIS2_PLACEMENT_3D ( 'NONE', #18165, #29355, #50666 ) ;
#62366=AXIS2_PLACEMENT_3D ( 'NONE', #20835, #14904, #57198 ) ;
#62414=VERTEX_POINT ( 'NONE', #46223 ) ;
#62420=CARTESIAN_POINT ( 'NONE',  ( 5.500000000000000000, 1.600000000000000089, 0.000000000000000000 ) ) ;
#62525=SHAPE_REPRESENTATION_RELATIONSHIP ( 'NONE' , 'NONE' ,  #46027, #46907 ) ;
#62559=PRODUCT_DEFINITION_CONTEXT ( 'detailed design', #43610, 'design' ) ;
#62590=VERTEX_POINT ( 'NONE', #64997 ) ;
#62614=ORIENTED_EDGE ( 'NONE', *, *, #10559, .F. ) ;
#62668=EDGE_CURVE ( 'NONE', #29897, #22158, #30826, .T. ) ;
#62706=VERTEX_POINT ( 'NONE', #23748 ) ;
#62714=DIRECTION ( 'NONE',  ( 0.000000000000000000, -0.1218274111675001492, -0.9925512993736016476 ) ) ;
#62747=AXIS2_PLACEMENT_3D ( 'NONE', #17935, #66161, #33324 ) ;
#62840=FACE_OUTER_BOUND ( 'NONE', #26051, .T. ) ;
#62965=LINE ( 'NONE', #67533, #25809 ) ;
#63027=EDGE_CURVE ( 'NONE', #24880, #47459, #25748, .T. ) ;
#63042=DIRECTION ( 'NONE',  ( 7.373249170895999531E-10, 7.373245149945000197E-10, -1.000000000000000000 ) ) ;
#63043=LINE ( 'NONE', #31600, #59200 ) ;
#63102=DIRECTION ( 'NONE',  ( 0.000000000000000000, -0.7071067811865474617, -0.7071067811865474617 ) ) ;
#63144=CYLINDRICAL_SURFACE ( 'NONE', #33355, 0.5500000000000000444 ) ;
#63179=DIRECTION ( 'NONE',  ( 0.000000000000000000, -1.000000000000000000, 0.000000000000000000 ) ) ;
#63226=DIRECTION ( 'NONE',  ( 0.000000000000000000, -0.1218274111675002463, 0.9925512993736016476 ) ) ;
#63233=CARTESIAN_POINT ( 'NONE',  ( 5.000000000000000000, -1.199999999999999956, -9.776630298829998011 ) ) ;
#63290=AXIS2_PLACEMENT_3D ( 'NONE', #39363, #3657, #13830 ) ;
#63339=EDGE_CURVE ( 'NONE', #17653, #7995, #37249, .T. ) ;
#63405=ORIENTED_EDGE ( 'NONE', *, *, #64369, .F. ) ;
#63509=PLANE ( 'NONE',  #68534 ) ;
#63545=EDGE_LOOP ( 'NONE', ( #17980, #14179, #28651, #9362, #56446 ) ) ;
#63702=VERTEX_POINT ( 'NONE', #57030 ) ;
#63739=AXIS2_PLACEMENT_3D ( 'NONE', #26100, #32043, #5110 ) ;
#63862=DIRECTION ( 'NONE',  ( 0.000000000000000000, -0.9620913858416644260, -0.2727272727272901376 ) ) ;
#63879=AXIS2_PLACEMENT_3D ( 'NONE', #907, #18029, #7518 ) ;
#63929=FACE_OUTER_BOUND ( 'NONE', #7629, .T. ) ;
#64006=LINE ( 'NONE', #10531, #25228 ) ;
#64049=EDGE_LOOP ( 'NONE', ( #41598, #5229, #60804, #46084 ) ) ;
#64075=VERTEX_POINT ( 'NONE', #22372 ) ;
#64153=EDGE_CURVE ( 'NONE', #41105, #12259, #39152, .T. ) ;
#64186=VERTEX_POINT ( 'NONE', #14647 ) ;
#64192=FACE_OUTER_BOUND ( 'NONE', #55661, .T. ) ;
#64193=DIRECTION ( 'NONE',  ( 0.000000000000000000, 0.2461538461537955413, 0.9692307692307821076 ) ) ;
#64274=VERTEX_POINT ( 'NONE', #59013 ) ;
#64291=ORIENTED_EDGE ( 'NONE', *, *, #6880, .F. ) ;
#64332=EDGE_CURVE ( 'NONE', #41105, #62590, #53078, .T. ) ;
#64369=EDGE_CURVE ( 'NONE', #43864, #57137, #19747, .T. ) ;
#64416=ORIENTED_EDGE ( 'NONE', *, *, #30611, .T. ) ;
#64430=FACE_OUTER_BOUND ( 'NONE', #63545, .T. ) ;
#64588=DIRECTION ( 'NONE',  ( 0.000000000000000000, -0.1218274111675002463, -0.9925512993736016476 ) ) ;
#64647=ORIENTED_EDGE ( 'NONE', *, *, #3689, .F. ) ;
#64650=VERTEX_POINT ( 'NONE', #50086 ) ;
#64733=PLANE ( 'NONE',  #50012 ) ;
#64740=CARTESIAN_POINT ( 'NONE',  ( 10.90000000000000036, -0.2500000000000000000, -9.776630298829998011 ) ) ;
#64761=EDGE_CURVE ( 'NONE', #18749, #42800, #30577, .T. ) ;
#64838=ORIENTED_EDGE ( 'NONE', *, *, #2664, .F. ) ;
#64847=ORIENTED_EDGE ( 'NONE', *, *, #6880, .T. ) ;
#64902=DIRECTION ( 'NONE',  ( 0.000000000000000000, -0.1218274111675001353, -0.9925512993736016476 ) ) ;
#64920=ORIENTED_EDGE ( 'NONE', *, *, #20313, .F. ) ;
#64994=ADVANCED_FACE ( 'NONE', ( #46719 ), #25726, .F. ) ;
#64997=CARTESIAN_POINT ( 'NONE',  ( 10.90000000000000036, -0.2500000000000000000, 9.776630298829998011 ) ) ;
#65016=EDGE_CURVE ( 'NONE', #44713, #38686, #43454, .T. ) ;
#65033=CARTESIAN_POINT ( 'NONE',  ( 5.500000000000000000, -0.2500000000000000000, -9.776630298829998011 ) ) ;
#65047=VERTEX_POINT ( 'NONE', #27289 ) ;
#65065=ORIENTED_EDGE ( 'NONE', *, *, #18539, .T. ) ;
#65069=VERTEX_POINT ( 'NONE', #37424 ) ;
#65103=EDGE_CURVE ( 'NONE', #65069, #17653, #32197, .T. ) ;
#65105=FACE_OUTER_BOUND ( 'NONE', #17716, .T. ) ;
#65205=FACE_OUTER_BOUND ( 'NONE', #51679, .T. ) ;
#65225=CIRCLE ( 'NONE', #40683, 10.80000000000000604 ) ;
#65235=CARTESIAN_POINT ( 'NONE',  ( 5.500000000000000000, 0.8000000000000000444, 3.149999999999999911 ) ) ;
#65246=SURFACE_STYLE_FILL_AREA ( #65594 ) ;
#65337=DIRECTION ( 'NONE',  ( 1.000000000000000000, 0.000000000000000000, 0.000000000000000000 ) ) ;
#65460=DIRECTION ( 'NONE',  ( 0.000000000000000000, 1.000000000000000000, 0.000000000000000000 ) ) ;
#65510=DIRECTION ( 'NONE',  ( 0.000000000000000000, 1.000000000000000000, 0.000000000000000000 ) ) ;
#65559=CARTESIAN_POINT ( 'NONE',  ( 5.200000000000000178, 0.000000000000000000, 0.000000000000000000 ) ) ;
#65594=FILL_AREA_STYLE ('',( #1629 ) ) ;
#65610=VERTEX_POINT ( 'NONE', #33490 ) ;
#65639=CONICAL_SURFACE ( 'NONE', #15400, 1.699999998954999869, 0.7853981633972997312 ) ;
#65757=LINE ( 'NONE', #28719, #39946 ) ;
#65778=DIRECTION ( 'NONE',  ( 0.000000000000000000, 1.000000000000000000, 0.000000000000000000 ) ) ;
#65882=DIRECTION ( 'NONE',  ( 0.000000000000000000, 0.000000000000000000, 1.000000000000000000 ) ) ;
#65933=( LENGTH_UNIT ( ) NAMED_UNIT ( * ) SI_UNIT ( .MILLI., .METRE. ) );
#65948=APPLICATION_CONTEXT ( 'automotive_design' ) ;
#66161=DIRECTION ( 'NONE',  ( 1.000000000000000000, 0.000000000000000000, 0.000000000000000000 ) ) ;
#66162=PLANE ( 'NONE',  #42245 ) ;
#66369=ORIENTED_EDGE ( 'NONE', *, *, #38570, .F. ) ;
#66437=ADVANCED_FACE ( 'NONE', ( #6398 ), #27748, .F. ) ;
#66472=CARTESIAN_POINT ( 'NONE',  ( 8.060840674114759352, -9.103590313266881395, -5.835422151730319307 ) ) ;
#66506=CARTESIAN_POINT ( 'NONE',  ( 10.90000000000000036, 0.000000000000000000, 0.000000000000000000 ) ) ;
#66611=DIRECTION ( 'NONE',  ( 0.000000000000000000, 0.2461538461537954858, -0.9692307692307821076 ) ) ;
#66642=DIRECTION ( 'NONE',  ( 1.000000000000000000, 0.000000000000000000, 0.000000000000000000 ) ) ;
#66711=ORIENTED_EDGE ( 'NONE', *, *, #63027, .T. ) ;
#66738=CARTESIAN_POINT ( 'NONE',  ( 5.200000000000000178, 0.8000000000000000444, 3.149999999999999911 ) ) ;
#66780=ORIENTED_EDGE ( 'NONE', *, *, #37701, .T. ) ;
#66936=CARTESIAN_POINT ( 'NONE',  ( 5.200000000000000178, 0.6646153846154000400, 2.616923076922999858 ) ) ;
#66945=ORIENTED_EDGE ( 'NONE', *, *, #61622, .T. ) ;
#67085=( NAMED_UNIT ( * ) SI_UNIT ( $, .STERADIAN. ) SOLID_ANGLE_UNIT ( ) );
#67218=DIRECTION ( 'NONE',  ( 1.000000000000000000, 0.000000000000000000, 0.000000000000000000 ) ) ;
#67221=CARTESIAN_POINT ( 'NONE',  ( 5.200000000963999724, 1.599999999036000098, -2.855877288059999651E-09 ) ) ;
#67237=DIRECTION ( 'NONE',  ( 1.000000000000000000, 0.000000000000000000, 0.000000000000000000 ) ) ;
#67250=AXIS2_PLACEMENT_3D ( 'NONE', #36924, #53000, #5096 ) ;
#67265=ORIENTED_EDGE ( 'NONE', *, *, #48129, .T. ) ;
#67272=DIRECTION ( 'NONE',  ( -3.827499907199999809E-10, -3.827498985732999890E-10, -1.000000000000000000 ) ) ;
#67277=CIRCLE ( 'NONE', #56111, 2.199999999999999734 ) ;
#67346=ORIENTED_EDGE ( 'NONE', *, *, #9564, .T. ) ;
#67413=DIRECTION ( 'NONE',  ( 0.000000000000000000, 1.000000000000000000, 0.000000000000000000 ) ) ;
#67422=AXIS2_PLACEMENT_3D ( 'NONE', #47871, #310, #16383 ) ;
#67430=EDGE_CURVE ( 'NONE', #8552, #29897, #51160, .T. ) ;
#67533=CARTESIAN_POINT ( 'NONE',  ( 5.200000002520999587, 0.6646153838164000627, -2.616923079727000001 ) ) ;
#67544=CARTESIAN_POINT ( 'NONE',  ( 7.000000000000000000, -9.735955015381000166, -5.735955015381000166 ) ) ;
#67556=CARTESIAN_POINT ( 'NONE',  ( 5.500000000000000000, 0.000000000000000000, 0.000000000000000000 ) ) ;
#67561=AXIS2_PLACEMENT_3D ( 'NONE', #59263, #33048, #53685 ) ;
#67568=ORIENTED_EDGE ( 'NONE', *, *, #3605, .F. ) ;
#67701=CARTESIAN_POINT ( 'NONE',  ( 5.000000000000000000, 0.8000000000000000444, -3.149999999999999911 ) ) ;
#67815=AXIS2_PLACEMENT_3D ( 'NONE', #68249, #30187, #8850 ) ;
#67829=AXIS2_PLACEMENT_3D ( 'NONE', #4668, #27048, #21108 ) ;
#67847=AXIS2_PLACEMENT_3D ( 'NONE', #2424, #56256, #3110 ) ;
#67928=CYLINDRICAL_SURFACE ( 'NONE', #38504, 1.449999999999999734 ) ;
#68020=B_SPLINE_CURVE_WITH_KNOTS ( 'NONE', 3,
 ( #1858, #13046, #60244, #12346 ),
 .UNSPECIFIED., .F., .F.,
 ( 4, 4 ),
 ( 0.000000000000000000, 1.000000000000000000 ),
 .UNSPECIFIED. ) ;
#68022=CARTESIAN_POINT ( 'NONE',  ( 10.90000000000000036, 0.2500000000000000000, 4.902439024389999567 ) ) ;
#68109=DIRECTION ( 'NONE',  ( 1.000000000000000000, 0.000000000000000000, 0.000000000000000000 ) ) ;
#68158=CARTESIAN_POINT ( 'NONE',  ( 7.000000000000000000, 0.8000000000000000444, -3.149999999999999911 ) ) ;
#68170=EDGE_CURVE ( 'NONE', #44713, #21934, #38608, .T. ) ;
#68192=LINE ( 'NONE', #26252, #21325 ) ;
#68215=LINE ( 'NONE', #41323, #42533 ) ;
#68249=CARTESIAN_POINT ( 'NONE',  ( 5.100000004521000108, 0.8000000000000000444, 3.149999999999999911 ) ) ;
#68338=CIRCLE ( 'NONE', #53831, 1.049999999999999822 ) ;
#68345=DIRECTION ( 'NONE',  ( -1.000000000000000000, -2.360367262211999706E-11, -1.096475580870000113E-09 ) ) ;
#68346=ORIENTED_EDGE ( 'NONE', *, *, #54778, .F. ) ;
#68405=ORIENTED_EDGE ( 'NONE', *, *, #37473, .F. ) ;
#68415=CARTESIAN_POINT ( 'NONE',  ( 7.102397164862999546, -0.2464401224313000349, -3.049949836518000001 ) ) ;
#68534=AXIS2_PLACEMENT_3D ( 'NONE', #11068, #32402, #47103 ) ;
#68587=CARTESIAN_POINT ( 'NONE',  ( 10.90000000000000036, 0.2500000000000000000, -4.902439024389999567 ) ) ;
#68670=DIRECTION ( 'NONE',  ( 0.000000000000000000, -0.8615889394142682844, 0.5076066385292812289 ) ) ;
#68795=VERTEX_POINT ( 'NONE', #18933 ) ;
#68800=DIRECTION ( 'NONE',  ( -0.7071067811866525998, 0.000000000000000000, -0.7071067811864425456 ) ) ;
#69097=CYLINDRICAL_SURFACE ( 'NONE', #46081, 2.200000000000000178 ) ;
#69102=CARTESIAN_POINT ( 'NONE',  ( 7.000000000000000000, 0.2708497377871000311, -3.000000000000000000 ) ) ;
#69104=VERTEX_POINT ( 'NONE', #34768 ) ;
#69148=ORIENTED_EDGE ( 'NONE', *, *, #63339, .F. ) ;
#69193=VECTOR ( 'NONE', #14442, 1000.000000000000000 ) ;
ENDSEC;
END-ISO-10303-21;
